ISO-10303-21;
HEADER;
FILE_DESCRIPTION (('STEP AP214'),
    '1' );
FILE_NAME ('hex flange bolt small_iso_ISO 4162 - M12 x 30 x 30-N.step',
    '2026-10-23T20:35:44',
    ( '' ),
    ( '' ),
    'SwSTEP 2.0',
    'SolidWorks 2025',
    '' );
FILE_SCHEMA (( 'AUTOMOTIVE_DESIGN' ));
ENDSEC;

DATA;
#3=EDGE_CURVE ( 'NONE', #4293, #4703, #7002, .T. ) ;
#4=CARTESIAN_POINT ( 'NONE',  ( 0.3581828924050324825, 0.3486337532542225226, 1.056976728655274672E-17 ) ) ;
#5=ORIENTED_EDGE ( 'NONE', *, *, #5535, .F. ) ;
#12=CARTESIAN_POINT ( 'NONE',  ( 0.3321019207957557895, 0.02907045490630093265, 0.2952755905511811330 ) ) ;
#28=AXIS2_PLACEMENT_3D ( 'NONE', #7517, #513, #2824 ) ;
#30=CARTESIAN_POINT ( 'NONE',  ( 0.3527008206095850751, 0.1709223649093223329, 0.2960462201727743214 ) ) ;
#32=CARTESIAN_POINT ( 'NONE',  ( 0.000000000000000000, -0.2557161625347750822, -0.1476377952755907330 ) ) ;
#39=ADVANCED_FACE ( 'NONE', ( #5518 ), #2011, .T. ) ;
#45=VECTOR ( 'NONE', #7259, 39.37007874015748143 ) ;
#55=CARTESIAN_POINT ( 'NONE',  ( 0.3336175750056032396, 0.2841290694830835850, -0.09842519685039363697 ) ) ;
#66=PLANE ( 'NONE',  #3064 ) ;
#68=PLANE ( 'NONE',  #1789 ) ;
#69=CARTESIAN_POINT ( 'NONE',  ( 0.01841426102874288775, 0.1429077274040485568, 0.2952755905511811330 ) ) ;
#74=CARTESIAN_POINT ( 'NONE',  ( 0.3528971332113848836, -0.3341112492250008503, 0.02492269209175877395 ) ) ;
#85=CARTESIAN_POINT ( 'NONE',  ( 0.3337350301074833991, 0.05917206666036364110, 0.2952755905511810774 ) ) ;
#93=FACE_OUTER_BOUND ( 'NONE', #3298, .T. ) ;
#97=EDGE_CURVE ( 'NONE', #6349, #6629, #5465, .T. ) ;
#107=CARTESIAN_POINT ( 'NONE',  ( 1.649606299212598381, 0.000000000000000000, 0.000000000000000000 ) ) ;
#115=B_SPLINE_CURVE_WITH_KNOTS ( 'NONE', 3,
 ( #6451, #6987, #1865, #683, #4728, #5964, #4691, #7061, #719 ),
 .UNSPECIFIED., .F., .F.,
 ( 4, 2, 1, 2, 4 ),
 ( 0.000000000000000000, 0.002165063509461098365, 0.004330127018922196730, 0.006495190528383293360, 0.008660254037844391725 ),
 .UNSPECIFIED. ) ;
#119=EDGE_LOOP ( 'NONE', ( #4224, #2865, #7199, #7516, #208 ) ) ;
#126=CARTESIAN_POINT ( 'NONE',  ( 0.3997746709170348356, 0.000000000000000000, 0.000000000000000000 ) ) ;
#134=EDGE_CURVE ( 'NONE', #2064, #5110, #3716, .T. ) ;
#142=CARTESIAN_POINT ( 'NONE',  ( 1.068462032678259234E-16, -0.2629500981735136689, -0.1351082512106133171 ) ) ;
#159=CARTESIAN_POINT ( 'NONE',  ( 0.01832242175888446414, 0.1844213691142423395, 0.2711239997950803393 ) ) ;
#163=CARTESIAN_POINT ( 'NONE',  ( 0.3426404862726872280, -0.2904653615686530466, 0.09998168480679490988 ) ) ;
#169=CARTESIAN_POINT ( 'NONE',  ( 0.3528850351813196951, 0.1886720902358826890, -0.2768301761068310274 ) ) ;
#177=CARTESIAN_POINT ( 'NONE',  ( 0.3997746709170348356, 5.668966274263039413E-17, 0.4629062255509093782 ) ) ;
#183=CARTESIAN_POINT ( 'NONE',  ( 0.3391216574607823775, -0.1954800165277041091, -0.2519698606119756268 ) ) ;
#188=CARTESIAN_POINT ( 'NONE',  ( 0.3391892065151629887, 0.1136516277932332897, 0.2952755905511810774 ) ) ;
#192=CARTESIAN_POINT ( 'NONE',  ( 0.3997746709170348356, 0.000000000000000000, -0.4629062255509093782 ) ) ;
#193=LINE ( 'NONE', #1323, #3033 ) ;
#194=CARTESIAN_POINT ( 'NONE',  ( -1.678725927747302331E-16, 0.2411939993270974525, 0.1727909197870958202 ) ) ;
#202=CARTESIAN_POINT ( 'NONE',  ( 0.3465697713329959906, -0.1180955399632931530, -0.2952755905511810774 ) ) ;
#204=ADVANCED_FACE ( 'NONE', ( #508 ), #6894, .T. ) ;
#205=CARTESIAN_POINT ( 'NONE',  ( 1.649606299212598381, 0.000000000000000000, 0.1982677165354330695 ) ) ;
#208=ORIENTED_EDGE ( 'NONE', *, *, #4312, .F. ) ;
#210=VERTEX_POINT ( 'NONE', #5171 ) ;
#216=CARTESIAN_POINT ( 'NONE',  ( 0.3387177083556158763, 0.2701412011613934516, 0.1226528954731279514 ) ) ;
#229=CARTESIAN_POINT ( 'NONE',  ( 0.3528971332113846615, 0.1886393090946605622, 0.2768874834731247514 ) ) ;
#239=CARTESIAN_POINT ( 'NONE',  ( 0.3411144883932946681, 0.06120045565151401717, -0.3014953316451452481 ) ) ;
#241=DIRECTION ( 'NONE',  ( 0.000000000000000000, 0.000000000000000000, 1.000000000000000000 ) ) ;
#258=ORIENTED_EDGE ( 'NONE', *, *, #7198, .F. ) ;
#262=CIRCLE ( 'NONE', #3188, 0.2362204724409449064 ) ;
#266=CARTESIAN_POINT ( 'NONE',  ( 0.3528850351813199171, 0.3340780101605773655, 0.02497973507596915402 ) ) ;
#275=CARTESIAN_POINT ( 'NONE',  ( 0.01832242175888456129, 0.3270109559553079359, -0.02415159075610075201 ) ) ;
#279=CARTESIAN_POINT ( 'NONE',  ( 1.055789886223273654E-16, -0.2411939993270979798, -0.1727909197870958757 ) ) ;
#293=ORIENTED_EDGE ( 'NONE', *, *, #4904, .T. ) ;
#310=B_SPLINE_CURVE_WITH_KNOTS ( 'NONE', 3,
 ( #2397, #7457, #2193, #4023, #4600, #2234, #4565, #4489 ),
 .UNSPECIFIED., .F., .F.,
 ( 4, 2, 2, 4 ),
 ( 0.004381617662950710798, 0.005472867551409541474, 0.006564117439868372150, 0.008746617216786031768 ),
 .UNSPECIFIED. ) ;
#311=EDGE_LOOP ( 'NONE', ( #1043, #2728, #1834, #6345 ) ) ;
#312=CARTESIAN_POINT ( 'NONE',  ( 0.02637295201093751290, -0.3409548833797009237, -9.138209691400258722E-18 ) ) ;
#314=ADVANCED_BREP_SHAPE_REPRESENTATION ( '', ( #1545, #5166 ), #1473 ) ;
#315=ORIENTED_EDGE ( 'NONE', *, *, #97, .T. ) ;
#317=CARTESIAN_POINT ( 'NONE',  ( 0.3322355029819564209, 0.06185644463604170890, -0.2952755905511810774 ) ) ;
#339=EDGE_CURVE ( 'NONE', #5905, #4449, #1926, .T. ) ;
#353=CARTESIAN_POINT ( 'NONE',  ( 0.3432736861146661322, -0.1846838951640047688, -0.2706692913385826404 ) ) ;
#354=ORIENTED_EDGE ( 'NONE', *, *, #7147, .F. ) ;
#385=CARTESIAN_POINT ( 'NONE',  ( 0.3485777078273626373, -0.2029921329169081246, -0.2518088348849962799 ) ) ;
#393=CARTESIAN_POINT ( 'NONE',  ( 0.3459463601587710602, -0.3157502742997210787, 0.04365566351110977683 ) ) ;
#396=TOROIDAL_SURFACE ( 'NONE', #4047, 0.4507874015748032370, 0.03543307086614166934 ) ;
#397=ORIENTED_EDGE ( 'NONE', *, *, #2431, .F. ) ;
#401=CARTESIAN_POINT ( 'NONE',  ( 0.3432736861146661878, -0.1420645347415422088, -0.2952755905511810774 ) ) ;
#418=CARTESIAN_POINT ( 'NONE',  ( 0.000000000000000000, 0.000000000000000000, 0.000000000000000000 ) ) ;
#435=CARTESIAN_POINT ( 'NONE',  ( 0.3487102105009307618, 0.2024297391849447236, -0.2527898980517343519 ) ) ;
#437=CARTESIAN_POINT ( 'NONE',  ( 0.3411151615605706455, -0.2917056203871725706, 0.09774174715353350917 ) ) ;
#445=CARTESIAN_POINT ( 'NONE',  ( 0.3306743754077733910, -4.012401740694386787E-16, -0.2952755905511810774 ) ) ;
#456=CARTESIAN_POINT ( 'NONE',  ( 0.02637295201093722841, 0.3409548833797004797, 3.882420715168025960E-18 ) ) ;
#460=LINE ( 'NONE', #561, #3345 ) ;
#464=UNCERTAINTY_MEASURE_WITH_UNIT (LENGTH_MEASURE( 1.000000000000000082E-05 ), #7315, 'distance_accuracy_value', 'NONE');
#468=CARTESIAN_POINT ( 'NONE',  ( 0.3426147637089221321, -0.05832033309504448121, 0.3015404986019939448 ) ) ;
#474=DIRECTION ( 'NONE',  ( -1.000000000000000000, -0.000000000000000000, -0.000000000000000000 ) ) ;
#478=B_SPLINE_CURVE_WITH_KNOTS ( 'NONE', 3,
 ( #3784, #4893, #6118, #2631, #4971, #1948 ),
 .UNSPECIFIED., .F., .F.,
 ( 4, 2, 4 ),
 ( 0.000000000000000000, 0.0001677595217559108194, 0.0003355190435118216388 ),
 .UNSPECIFIED. ) ;
#482=CARTESIAN_POINT ( 'NONE',  ( 0.02637295201093751290, -0.3409548833797009237, -9.138209691400258722E-18 ) ) ;
#483=ORIENTED_EDGE ( 'NONE', *, *, #6552, .F. ) ;
#484=EDGE_CURVE ( 'NONE', #2382, #4304, #1169, .T. ) ;
#485=CARTESIAN_POINT ( 'NONE',  ( 0.3483227611829849413, -0.3409548833797009237, 0.000000000000000000 ) ) ;
#499=CIRCLE ( 'NONE', #5364, 0.4629062255509093782 ) ;
#504=FACE_OUTER_BOUND ( 'NONE', #119, .T. ) ;
#508=FACE_OUTER_BOUND ( 'NONE', #2139, .T. ) ;
#509=CARTESIAN_POINT ( 'NONE',  ( 0.3425764178929370796, -0.2900721174007588332, -0.1006592143205869427 ) ) ;
#513=DIRECTION ( 'NONE',  ( -1.000000000000000000, -0.000000000000000000, -0.000000000000000000 ) ) ;
#521=ORIENTED_EDGE ( 'NONE', *, *, #1115, .F. ) ;
#543=ORIENTED_EDGE ( 'NONE', *, *, #1482, .T. ) ;
#550=ORIENTED_EDGE ( 'NONE', *, *, #3088, .T. ) ;
#556=LINE ( 'NONE', #177, #2443 ) ;
#561=CARTESIAN_POINT ( 'NONE',  ( 0.000000000000000000, 0.000000000000000000, 0.2362204724409449064 ) ) ;
#585=ORIENTED_EDGE ( 'NONE', *, *, #5580, .T. ) ;
#588=CARTESIAN_POINT ( 'NONE',  ( 0.3411158341578399145, -0.06121148758009550134, 0.3014953708557878698 ) ) ;
#593=CARTESIAN_POINT ( 'NONE',  ( 0.3336175750056031841, 0.2273032555864666071, -0.1968503937007874127 ) ) ;
#606=CARTESIAN_POINT ( 'NONE',  ( 0.3581828924050324825, -0.1743168766271116221, -0.3019256869348722061 ) ) ;
#640=AXIS2_PLACEMENT_3D ( 'NONE', #5169, #1024, #2176 ) ;
#647=CARTESIAN_POINT ( 'NONE',  ( 0.02637295201093703412, 0.1704774416898499345, 0.2952755905511810774 ) ) ;
#674=ORIENTED_EDGE ( 'NONE', *, *, #6552, .T. ) ;
#676=FACE_OUTER_BOUND ( 'NONE', #4781, .T. ) ;
#683=CARTESIAN_POINT ( 'NONE',  ( 0.3336175750056032396, 0.2273032555864667459, 0.1968503937007873295 ) ) ;
#687=CARTESIAN_POINT ( 'NONE',  ( 0.000000000000000000, 0.2557161625347750267, 0.1476377952755908163 ) ) ;
#708=DIRECTION ( 'NONE',  ( 0.000000000000000000, 0.000000000000000000, 1.000000000000000000 ) ) ;
#712=CARTESIAN_POINT ( 'NONE',  ( 0.3487102105009288744, -0.3201373431253433655, -0.04891434758976972302 ) ) ;
#719=CARTESIAN_POINT ( 'NONE',  ( 0.3483227611829848303, 0.3409548833797004797, 0.000000000000000000 ) ) ;
#722=CARTESIAN_POINT ( 'NONE',  ( 0.000000000000000000, 0.000000000000000000, -0.2952755905511810774 ) ) ;
#725=VERTEX_POINT ( 'NONE', #1380 ) ;
#733=VERTEX_POINT ( 'NONE', #5947 ) ;
#738=CARTESIAN_POINT ( 'NONE',  ( 0.3459468362671123676, -0.1200707489736706907, 0.2952755905511811885 ) ) ;
#746=CARTESIAN_POINT ( 'NONE',  ( 0.01834252172841674411, -0.3270457701237520221, -0.02409129084753309710 ) ) ;
#748=CIRCLE ( 'NONE', #7336, 0.2952755905511810774 ) ;
#753=VECTOR ( 'NONE', #7293, 39.37007874015748143 ) ;
#764=CARTESIAN_POINT ( 'NONE',  ( 1.611653543307086212, 0.000000000000000000, 0.2362204724409449064 ) ) ;
#779=CARTESIAN_POINT ( 'NONE',  ( 0.3531511627980717938, 0.3349346966101464096, 0.02350890366534340997 ) ) ;
#787=PRODUCT_DEFINITION ( 'UNKNOWN', '', #6798, #7097 ) ;
#798=CARTESIAN_POINT ( 'NONE',  ( 1.170506159394721758E-17, 0.02884736746562922144, 0.2952755905511810774 ) ) ;
#803=CARTESIAN_POINT ( 'NONE',  ( 0.000000000000000000, 0.000000000000000000, -0.2952755905511810774 ) ) ;
#815=( BOUNDED_SURFACE ( )  B_SPLINE_SURFACE ( 3, 2, ( 
 ( #7486, #6848, #2145 ),
 ( #1604, #2823, #6278 ),
 ( #5176, #998, #3908 ),
 ( #4479, #5135, #3332 ),
 ( #2752, #5093, #6921 ),
 ( #5783, #2184, #435 ),
 ( #1065, #7447, #2260 ),
 ( #2223, #4518, #3950 ) ),
 .UNSPECIFIED., .F., .F., .F. ) 
 B_SPLINE_SURFACE_WITH_KNOTS ( ( 4, 2, 2, 4 ),
 ( 3, 3 ),
 ( 0.03551798592901333346, 0.03994769179990642627, 0.04216254473535296921, 0.04437739767079951908 ),
 ( 0.000000000000000000, 1.000000000000000000 ),
 .UNSPECIFIED. ) 
 GEOMETRIC_REPRESENTATION_ITEM ( )  RATIONAL_B_SPLINE_SURFACE ( (
 ( 1.000000000000000000, 0.8047781103519390244, 1.000000000000000000),
 ( 1.000000000000000000, 0.8123785826175446978, 1.000000000000000000),
 ( 1.000000000000000000, 0.8190671539027887249, 1.000000000000000000),
 ( 1.000000000000000000, 0.8191932076453414258, 1.000000000000000000),
 ( 1.000000000000000000, 0.8176085094066379844, 1.000000000000000000),
 ( 1.000000000000000000, 0.8122955484014008354, 1.000000000000000000),
 ( 1.000000000000000000, 0.8086308001280824165, 1.000000000000000000),
 ( 1.000000000000000000, 0.8047712537969731184, 1.000000000000000000) ) ) 
 REPRESENTATION_ITEM ( '' )  SURFACE ( )  );
#824=( NAMED_UNIT ( * ) SI_UNIT ( $, .STERADIAN. ) SOLID_ANGLE_UNIT ( ) );
#826=DIRECTION ( 'NONE',  ( -1.000000000000000000, -0.000000000000000000, -0.000000000000000000 ) ) ;
#836=CARTESIAN_POINT ( 'NONE',  ( 0.3485373078438442351, 0.3194486952732363827, 0.05009812457233156491 ) ) ;
#846=CARTESIAN_POINT ( 'NONE',  ( 0.3459458835994366765, 0.1200656956960832605, -0.2952755905511810774 ) ) ;
#852=ADVANCED_FACE ( 'NONE', ( #6737 ), #5603, .F. ) ;
#854=CARTESIAN_POINT ( 'NONE',  ( 0.01836325778988931109, -0.1427310470019619582, -0.2952755905511810774 ) ) ;
#857=CARTESIAN_POINT ( 'NONE',  ( 0.3409812221349194372, 0.2754857644942527717, 0.1258275564122752488 ) ) ;
#865=( LENGTH_UNIT ( ) NAMED_UNIT ( * ) SI_UNIT ( $, .METRE. ) );
#868=DIRECTION ( 'NONE',  ( 0.000000000000000000, 0.000000000000000000, -1.000000000000000000 ) ) ;
#878=ORIENTED_EDGE ( 'NONE', *, *, #1482, .F. ) ;
#885=AXIS2_PLACEMENT_3D ( 'NONE', #4491, #6900, #4130 ) ;
#887=ORIENTED_EDGE ( 'NONE', *, *, #2928, .F. ) ;
#900=EDGE_CURVE ( 'NONE', #6925, #7325, #6669, .T. ) ;
#912=CARTESIAN_POINT ( 'NONE',  ( 0.01171324505787554003, 0.3130206113228969356, 0.04838357847483527874 ) ) ;
#916=CARTESIAN_POINT ( 'NONE',  ( 0.01168997831664865018, 0.3129651733100085598, -0.04847959992982851796 ) ) ;
#917=CARTESIAN_POINT ( 'NONE',  ( 0.3391211773724056577, 0.1204696997606904962, -0.2952755905511810774 ) ) ;
#919=CARTESIAN_POINT ( 'NONE',  ( 0.000000000000000000, 0.000000000000000000, 0.000000000000000000 ) ) ;
#939=B_SPLINE_CURVE_WITH_KNOTS ( 'NONE', 3,
 ( #485, #5690, #2265, #6287, #5309, #2800, #7383, #5886, #5184 ),
 .UNSPECIFIED., .F., .F.,
 ( 4, 2, 1, 2, 4 ),
 ( 0.000000000000000000, 0.002165063509461098799, 0.004330127018922199332, 0.006495190528383298564, 0.008660254037844398664 ),
 .UNSPECIFIED. ) ;
#952=B_SPLINE_CURVE_WITH_KNOTS ( 'NONE', 3,
 ( #1363, #798, #4160, #2396, #69, #647 ),
 .UNSPECIFIED., .F., .F.,
 ( 4, 2, 4 ),
 ( 0.01227927579290655560, 0.01447189347357576844, 0.01666451115424498128 ),
 .UNSPECIFIED. ) ;
#954=CARTESIAN_POINT ( 'NONE',  ( 0.000000000000000000, 0.3409548833797004797, 2.164902785881980513E-17 ) ) ;
#956=DIRECTION ( 'NONE',  ( -1.000000000000000000, -0.000000000000000000, -0.000000000000000000 ) ) ;
#962=CARTESIAN_POINT ( 'NONE',  ( 0.4685039370078740717, 0.1704774416898499345, 0.2952755905511810774 ) ) ;
#968=CARTESIAN_POINT ( 'NONE',  ( 0.4685039370078740717, 0.1704774416898497680, -0.2952755905511810774 ) ) ;
#990=ORIENTED_EDGE ( 'NONE', *, *, #5535, .T. ) ;
#992=CARTESIAN_POINT ( 'NONE',  ( 0.3528822938286764188, -0.1453909600788099998, 0.3018098512751525853 ) ) ;
#998=CARTESIAN_POINT ( 'NONE',  ( 0.3388536909602617997, 0.2864058322153591463, -0.09448172812127442199 ) ) ;
#1002=CARTESIAN_POINT ( 'NONE',  ( 0.000000000000000000, 0.000000000000000000, -0.2952755905511810774 ) ) ;
#1015=LINE ( 'NONE', #1730, #5372 ) ;
#1022=CARTESIAN_POINT ( 'NONE',  ( 0.02637295201093722841, 0.3409548833797004797, 3.882420715168025960E-18 ) ) ;
#1024=DIRECTION ( 'NONE',  ( 1.000000000000000000, 0.000000000000000000, 0.000000000000000000 ) ) ;
#1034=CARTESIAN_POINT ( 'NONE',  ( 0.3306743754077736130, -0.2557161625347756373, -0.1476377952755904555 ) ) ;
#1037=CARTESIAN_POINT ( 'NONE',  ( 0.3531511627980793433, -0.1878266560944103492, 0.2783075040405565415 ) ) ;
#1042=CARTESIAN_POINT ( 'NONE',  ( 0.3483227611829846082, 0.1704774416898497680, -0.2952755905511810774 ) ) ;
#1043=ORIENTED_EDGE ( 'NONE', *, *, #3, .F. ) ;
#1060=CARTESIAN_POINT ( 'NONE',  ( 0.3496875133419357629, -0.1780312604149854316, -0.2952755905511810774 ) ) ;
#1065=CARTESIAN_POINT ( 'NONE',  ( 0.3442723180357227797, 0.1814473180894613513, -0.2762752072743030474 ) ) ;
#1090=DIRECTION ( 'NONE',  ( 1.000000000000000000, 0.000000000000000000, 0.000000000000000000 ) ) ;
#1098=ORIENTED_EDGE ( 'NONE', *, *, #4460, .F. ) ;
#1102=CARTESIAN_POINT ( 'NONE',  ( 0.3391892065151629332, 0.1136516277932330399, -0.2952755905511810774 ) ) ;
#1111=ADVANCED_FACE ( 'NONE', ( #4245 ), #396, .T. ) ;
#1115=EDGE_CURVE ( 'NONE', #4304, #4703, #3678, .T. ) ;
#1117=FACE_OUTER_BOUND ( 'NONE', #3223, .T. ) ;
#1126=CARTESIAN_POINT ( 'NONE',  ( 0.4685039370078740717, -0.3409548833797009237, 0.000000000000000000 ) ) ;
#1127=ORIENTED_EDGE ( 'NONE', *, *, #1920, .F. ) ;
#1135=CARTESIAN_POINT ( 'NONE',  ( 0.4685039370078740717, 5.594759879304195485E-17, -0.4507874015748032370 ) ) ;
#1145=CARTESIAN_POINT ( 'NONE',  ( 0.4685039370078740717, 0.3409548833797004797, 2.164902785881980513E-17 ) ) ;
#1160=CARTESIAN_POINT ( 'NONE',  ( 0.3410249605999410294, 1.062103031354818709E-12, 0.3014927230551906479 ) ) ;
#1165=ORIENTED_EDGE ( 'NONE', *, *, #5580, .F. ) ;
#1169=B_SPLINE_CURVE_WITH_KNOTS ( 'NONE', 3,
 ( #1939, #6254, #3965, #2128, #6863, #7207 ),
 .UNSPECIFIED., .F., .F.,
 ( 4, 2, 4 ),
 ( 0.000000000000000000, 0.002233368740102889029, 0.004466737480205778058 ),
 .UNSPECIFIED. ) ;
#1170=VERTEX_POINT ( 'NONE', #6973 ) ;
#1176=CARTESIAN_POINT ( 'NONE',  ( 0.3403859949404050012, 0.05880135802647309951, 0.2952755905511811330 ) ) ;
#1178=DIRECTION ( 'NONE',  ( 0.000000000000000000, 0.000000000000000000, -1.000000000000000000 ) ) ;
#1182=CARTESIAN_POINT ( 'NONE',  ( 0.3306743754077735575, 0.2557161625347751932, -0.1476377952755904832 ) ) ;
#1207=ORIENTED_EDGE ( 'NONE', *, *, #7509, .F. ) ;
#1212=FACE_OUTER_BOUND ( 'NONE', #6387, .T. ) ;
#1218=CARTESIAN_POINT ( 'NONE',  ( 0.3442721343065135997, 0.1485366976410457951, 0.2952755905511810774 ) ) ;
#1223=VECTOR ( 'NONE', #2809, 39.37007874015748143 ) ;
#1224=ORIENTED_EDGE ( 'NONE', *, *, #2013, .T. ) ;
#1238=DIRECTION ( 'NONE',  ( -1.000000000000000000, -0.000000000000000000, -0.000000000000000000 ) ) ;
#1239=CARTESIAN_POINT ( 'NONE',  ( 0.3426022948973417859, 0.05819196463765207578, 0.3015401604570892014 ) ) ;
#1243=AXIS2_PLACEMENT_3D ( 'NONE', #5009, #4546, #7326 ) ;
#1245=CARTESIAN_POINT ( 'NONE',  ( 0.3581828924050323715, -0.1743168766271109560, 0.3019256869348722616 ) ) ;
#1260=MECHANICAL_DESIGN_GEOMETRIC_PRESENTATION_REPRESENTATION('',(#5795),#4688);
#1263=CARTESIAN_POINT ( 'NONE',  ( 0.3426140154788509529, 0.05854580700589206294, 0.3015405874046677703 ) ) ;
#1269=CARTESIAN_POINT ( 'NONE',  ( 0.3321022367506965556, -0.2702568778840481745, -0.1224525375122541698 ) ) ;
#1277=DIRECTION ( 'NONE',  ( -0.000000000000000000, 0.000000000000000000, 1.000000000000000000 ) ) ;
#1285=CARTESIAN_POINT ( 'NONE',  ( 0.3485373078438442351, -0.2031105961982146157, 0.2516016230262508313 ) ) ;
#1287=ORIENTED_EDGE ( 'NONE', *, *, #1336, .T. ) ;
#1298=CARTESIAN_POINT ( 'NONE',  ( 0.3496779098333545610, -0.1779789496721726760, 0.2952755905511811330 ) ) ;
#1299=SHAPE_DEFINITION_REPRESENTATION ( #1469, #7075 ) ;
#1305=AXIS2_PLACEMENT_3D ( 'NONE', #5939, #4127, #3483 ) ;
#1311=CARTESIAN_POINT ( 'NONE',  ( 0.3510872220067592364, -0.3295092824291515621, -0.01982436236955561690 ) ) ;
#1314=CARTESIAN_POINT ( 'NONE',  ( 0.3581828924050327045, -0.3486337532542230222, -1.123169198254405176E-18 ) ) ;
#1318=CARTESIAN_POINT ( 'NONE',  ( 0.4685039370078740717, 0.000000000000000000, 0.000000000000000000 ) ) ;
#1323=CARTESIAN_POINT ( 'NONE',  ( 1.649606299212598381, 0.000000000000000000, 0.1982677165354330695 ) ) ;
#1336=EDGE_CURVE ( 'NONE', #733, #3843, #3029, .T. ) ;
#1339=CARTESIAN_POINT ( 'NONE',  ( 0.3505601438611543053, -0.3409548833797009237, 1.488710258487716964E-17 ) ) ;
#1344=ORIENTED_EDGE ( 'NONE', *, *, #1880, .F. ) ;
#1345=ADVANCED_FACE ( 'NONE', ( #2588 ), #3837, .T. ) ;
#1363=CARTESIAN_POINT ( 'NONE',  ( 0.000000000000000000, 2.957312202238506242E-17, 0.2952755905511810774 ) ) ;
#1366=DIRECTION ( 'NONE',  ( -1.000000000000000000, -0.000000000000000000, -0.000000000000000000 ) ) ;
#1371=CARTESIAN_POINT ( 'NONE',  ( 0.3403868552871069930, -0.05881191477760600722, -0.2952755905511810774 ) ) ;
#1373=TOROIDAL_SURFACE ( 'NONE', #3455, 0.4507874015748032370, 0.03543307086614166934 ) ;
#1380=CARTESIAN_POINT ( 'NONE',  ( 0.000000000000000000, -0.2557161625347748601, 0.1476377952755911216 ) ) ;
#1385=AXIS2_PLACEMENT_3D ( 'NONE', #2670, #956, #2632 ) ;
#1388=VERTEX_POINT ( 'NONE', #5165 ) ;
#1397=ADVANCED_FACE ( 'NONE', ( #3618 ), #7475, .F. ) ;
#1403=ORIENTED_EDGE ( 'NONE', *, *, #3403, .F. ) ;
#1435=APPLICATION_CONTEXT ( 'automotive_design' ) ;
#1439=EDGE_CURVE ( 'NONE', #2064, #4413, #4934, .T. ) ;
#1440=DIRECTION ( 'NONE',  ( 0.000000000000000000, 0.000000000000000000, -1.000000000000000000 ) ) ;
#1441=EDGE_CURVE ( 'NONE', #5853, #4821, #460, .T. ) ;
#1443=ORIENTED_EDGE ( 'NONE', *, *, #484, .F. ) ;
#1448=CARTESIAN_POINT ( 'NONE',  ( 0.02637295201093723881, -0.1704774416898505729, -0.2952755905511810774 ) ) ;
#1452=ORIENTED_EDGE ( 'NONE', *, *, #6784, .T. ) ;
#1458=CARTESIAN_POINT ( 'NONE',  ( 1.611653543307086212, 0.000000000000000000, 0.000000000000000000 ) ) ;
#1469=PRODUCT_DEFINITION_SHAPE ( 'NONE', 'NONE',  #787 ) ;
#1473=( GEOMETRIC_REPRESENTATION_CONTEXT ( 3 ) GLOBAL_UNCERTAINTY_ASSIGNED_CONTEXT ( ( #5340 ) ) GLOBAL_UNIT_ASSIGNED_CONTEXT ( ( #4919, #4836, #824 ) ) REPRESENTATION_CONTEXT ( 'NONE', 'WORKASPACE' ) );
#1475=CARTESIAN_POINT ( 'NONE',  ( 0.3496779450092586949, 0.1779791412978203036, -0.2952755905511810774 ) ) ;
#1479=ORIENTED_EDGE ( 'NONE', *, *, #900, .T. ) ;
#1482=EDGE_CURVE ( 'NONE', #725, #7262, #3582, .T. ) ;
#1483=EDGE_CURVE ( 'NONE', #1950, #7325, #2210, .T. ) ;
#1501=CARTESIAN_POINT ( 'NONE',  ( 0.3483227611829848303, -0.1704774416898505729, -0.2952755905511810774 ) ) ;
#1519=ORIENTED_EDGE ( 'NONE', *, *, #4662, .T. ) ;
#1528=CARTESIAN_POINT ( 'NONE',  ( 0.3465694189147047188, 0.3147628225698786419, 0.04536598007754604617 ) ) ;
#1545=MANIFOLD_SOLID_BREP ( 'FlangeHexFillet', #4204 ) ;
#1548=CARTESIAN_POINT ( 'NONE',  ( 0.3505601438611538057, 0.1704774416898496292, -0.2952755905511812995 ) ) ;
#1553=ORIENTED_EDGE ( 'NONE', *, *, #5622, .F. ) ;
#1559=CARTESIAN_POINT ( 'NONE',  ( 0.3336175750056034062, -0.2273032555864673288, -0.1968503937007873295 ) ) ;
#1570=CARTESIAN_POINT ( 'NONE',  ( 0.002513486811083624848, -0.2845799557467911245, 0.09764423893321799719 ) ) ;
#1581=CARTESIAN_POINT ( 'NONE',  ( 0.3527006543068525457, -0.1709223289430796822, -0.2960461578774135627 ) ) ;
#1588=EDGE_CURVE ( 'NONE', #5110, #3761, #6867, .T. ) ;
#1593=CARTESIAN_POINT ( 'NONE',  ( 0.01834252172841645614, 0.3270457701237517445, 0.02409129084753309363 ) ) ;
#1604=CARTESIAN_POINT ( 'NONE',  ( 0.3391216574608371670, 0.3159523085418723398, -0.04330572993916122215 ) ) ;
#1605=CARTESIAN_POINT ( 'NONE',  ( 0.3565422270302656127, -0.1673297761639321035, 0.3007275071673038980 ) ) ;
#1618=CIRCLE ( 'NONE', #28, 0.1982677165354330695 ) ;
#1632=ORIENTED_EDGE ( 'NONE', *, *, #7103, .T. ) ;
#1634=CARTESIAN_POINT ( 'NONE',  ( 0.3581828924050327045, -0.3486337532542230222, -1.123169198254405176E-18 ) ) ;
#1655=ORIENTED_EDGE ( 'NONE', *, *, #6907, .T. ) ;
#1671=DIRECTION ( 'NONE',  ( 0.000000000000000000, 0.000000000000000000, -1.000000000000000000 ) ) ;
#1677=EDGE_LOOP ( 'NONE', ( #6252, #2486, #6667, #6069 ) ) ;
#1679=CARTESIAN_POINT ( 'NONE',  ( 0.3321022367507227568, -0.2411754471855062087, 0.1728230530389214537 ) ) ;
#1685=ADVANCED_FACE ( 'NONE', ( #2376 ), #3027, .T. ) ;
#1689=CIRCLE ( 'NONE', #1796, 0.2952755905511810774 ) ;
#1712=ORIENTED_EDGE ( 'NONE', *, *, #6995, .T. ) ;
#1724=ORIENTED_EDGE ( 'NONE', *, *, #2492, .F. ) ;
#1730=CARTESIAN_POINT ( 'NONE',  ( 0.4685039370078740717, 0.3409548833797004797, 0.000000000000000000 ) ) ;
#1735=CARTESIAN_POINT ( 'NONE',  ( 0.4685039370078740717, 0.1704774416898497680, -0.2952755905511810774 ) ) ;
#1739=CARTESIAN_POINT ( 'NONE',  ( 0.3505602286436571013, 0.1704774416898499345, 0.2952755905511810774 ) ) ;
#1746=ORIENTED_EDGE ( 'NONE', *, *, #4312, .T. ) ;
#1749=CARTESIAN_POINT ( 'NONE',  ( 0.3410425348215777031, 0.2759054741781710729, -0.1251041708914593098 ) ) ;
#1750=ORIENTED_EDGE ( 'NONE', *, *, #339, .T. ) ;
#1759=EDGE_LOOP ( 'NONE', ( #5817, #3961, #7254, #2648, #1443 ) ) ;
#1763=PLANE ( 'NONE',  #2708 ) ;
#1779=ORIENTED_EDGE ( 'NONE', *, *, #4207, .F. ) ;
#1789=AXIS2_PLACEMENT_3D ( 'NONE', #1126, #7023, #2439 ) ;
#1790=DIRECTION ( 'NONE',  ( 0.000000000000000000, 0.000000000000000000, 1.000000000000000000 ) ) ;
#1794=CARTESIAN_POINT ( 'NONE',  ( 0.3565422412058069090, 0.1767728485866832400, 0.2952755905511811330 ) ) ;
#1796=AXIS2_PLACEMENT_3D ( 'NONE', #6898, #3995, #5104 ) ;
#1799=ORIENTED_EDGE ( 'NONE', *, *, #97, .F. ) ;
#1801=ADVANCED_FACE ( 'NONE', ( #6102 ), #5769, .F. ) ;
#1813=B_SPLINE_CURVE_WITH_KNOTS ( 'NONE', 3,
 ( #3089, #266, #836, #3780, #6114, #4319, #7212, #2483, #229, #2550 ),
 .UNSPECIFIED., .F., .F.,
 ( 4, 2, 2, 2, 4 ),
 ( 0.000000000000000000, 0.002239656411828510555, 0.004479312823657022845, 0.006718969235485534701, 0.008958625647314047424 ),
 .UNSPECIFIED. ) ;
#1817=CARTESIAN_POINT ( 'NONE',  ( 0.3581828924050323715, 0.1743168766271109560, 0.3019256869348722616 ) ) ;
#1818=LINE ( 'NONE', #4152, #3661 ) ;
#1822=CARTESIAN_POINT ( 'NONE',  ( 0.3485616995351332181, 0.1165012447190262312, 0.3017003685801735724 ) ) ;
#1828=CARTESIAN_POINT ( 'NONE',  ( 0.3485534891173983629, 0.1164145375797932258, -0.3017001449125945034 ) ) ;
#1833=CARTESIAN_POINT ( 'NONE',  ( 0.3426404862726871725, 0.2904653615686527135, -0.09998168480679492376 ) ) ;
#1834=ORIENTED_EDGE ( 'NONE', *, *, #4207, .T. ) ;
#1842=CARTESIAN_POINT ( 'NONE',  ( 0.3409809061799574659, 0.02876216262209277050, 0.3014914394333951253 ) ) ;
#1855=CARTESIAN_POINT ( 'NONE',  ( 0.3459463601586513781, -0.1956820507697304701, -0.2516199270400212851 ) ) ;
#1865=CARTESIAN_POINT ( 'NONE',  ( 0.3391892065151629332, 0.1988903486381583818, 0.2460629921259842312 ) ) ;
#1867=PLANE ( 'NONE',  #4389 ) ;
#1880=EDGE_CURVE ( 'NONE', #5498, #4759, #939, .T. ) ;
#1913=CARTESIAN_POINT ( 'NONE',  ( 0.3485777078273626928, -0.3195689143662223120, 0.04989192643193118837 ) ) ;
#1914=B_SPLINE_CURVE_WITH_KNOTS ( 'NONE', 3,
 ( #7445, #353, #2143, #1559, #1034, #6198, #6806, #3404, #5710 ),
 .UNSPECIFIED., .F., .F.,
 ( 4, 2, 1, 2, 4 ),
 ( 0.000000000000000000, 0.002165063509461096630, 0.004330127018922193260, 0.006495190528383289023, 0.008660254037844388256 ),
 .UNSPECIFIED. ) ;
#1916=FACE_OUTER_BOUND ( 'NONE', #4742, .T. ) ;
#1919=EDGE_CURVE ( 'NONE', #6629, #210, #310, .T. ) ;
#1920=EDGE_CURVE ( 'NONE', #3692, #725, #1689, .T. ) ;
#1926=B_SPLINE_CURVE_WITH_KNOTS ( 'NONE', 3,
 ( #4725, #1739, #30, #5264, #2434, #1817 ),
 .UNSPECIFIED., .F., .F.,
 ( 4, 2, 4 ),
 ( 0.000000000000000000, 0.0001677595217559110904, 0.0003355190435118221809 ),
 .UNSPECIFIED. ) ;
#1938=B_SPLINE_CURVE_WITH_KNOTS ( 'NONE', 3,
 ( #5001, #7251, #4885, #6718, #2625, #2023, #188, #4315, #1940 ),
 .UNSPECIFIED., .F., .F.,
 ( 4, 2, 1, 2, 4 ),
 ( 0.000000000000000000, 0.002165063509461094028, 0.004330127018922188056, 0.006495190528383282084, 0.008660254037844376113 ),
 .UNSPECIFIED. ) ;
#1939=CARTESIAN_POINT ( 'NONE',  ( 0.3581828924050324825, -0.1743168766271116221, -0.3019256869348722061 ) ) ;
#1940=CARTESIAN_POINT ( 'NONE',  ( 0.3483227611829846637, 0.1704774416898499345, 0.2952755905511810774 ) ) ;
#1945=CARTESIAN_POINT ( 'NONE',  ( 0.02637295201093703412, 0.1704774416898499345, 0.2952755905511810774 ) ) ;
#1948=CARTESIAN_POINT ( 'NONE',  ( 0.3581828924050324825, 0.3486337532542225226, 1.056976728655274672E-17 ) ) ;
#1950=VERTEX_POINT ( 'NONE', #4733 ) ;
#1951=CARTESIAN_POINT ( 'NONE',  ( 0.3510874053966554498, -0.1475872118127406207, -0.2952755905511810774 ) ) ;
#1965=CARTESIAN_POINT ( 'NONE',  ( 0.3321022367506963890, 0.2702568778840441777, 0.1224525375122600818 ) ) ;
#1970=ORIENTED_EDGE ( 'NONE', *, *, #134, .T. ) ;
#1974=EDGE_CURVE ( 'NONE', #3692, #7446, #2186, .T. ) ;
#1995=CARTESIAN_POINT ( 'NONE',  ( 1.649606299212598381, 2.428079244293728657E-17, -0.1982677165354330695 ) ) ;
#2002=ORIENTED_EDGE ( 'NONE', *, *, #3456, .T. ) ;
#2005=B_SPLINE_CURVE_WITH_KNOTS ( 'NONE', 3,
 ( #6997, #169, #4631, #5246, #7032, #1749, #1833, #6513, #6962, #4 ),
 .UNSPECIFIED., .F., .F.,
 ( 4, 2, 2, 2, 4 ),
 ( 0.000000000000000000, 0.002239656411828510989, 0.004479312823657021977, 0.006718969235485534701, 0.008958625647314047424 ),
 .UNSPECIFIED. ) ;
#2007=CARTESIAN_POINT ( 'NONE',  ( 0.3442723180356496160, 0.3299850069800976948, 0.01900038327686272982 ) ) ;
#2008=ORIENTED_EDGE ( 'NONE', *, *, #7250, .T. ) ;
#2011=CONICAL_SURFACE ( 'NONE', #1385, 0.1982677165354330695, 0.7853981633974415066 ) ;
#2013=EDGE_CURVE ( 'NONE', #1170, #7446, #4141, .T. ) ;
#2014=ORIENTED_EDGE ( 'NONE', *, *, #6907, .F. ) ;
#2015=B_SPLINE_CURVE_WITH_KNOTS ( 'NONE', 3,
 ( #5849, #2926, #7067, #1828, #3050, #4163 ),
 .UNSPECIFIED., .F., .F.,
 ( 4, 2, 4 ),
 ( 0.004466737480205778058, 0.006712681563759909271, 0.008958625647314040485 ),
 .UNSPECIFIED. ) ;
#2018=( NAMED_UNIT ( * ) PLANE_ANGLE_UNIT ( ) SI_UNIT ( $, .RADIAN. ) );
#2023=CARTESIAN_POINT ( 'NONE',  ( 0.3336175750056032951, 0.05682581389661665178, 0.2952755905511811885 ) ) ;
#2025=DIRECTION ( 'NONE',  ( 1.000000000000000000, 0.000000000000000000, 0.000000000000000000 ) ) ;
#2026=CARTESIAN_POINT ( 'NONE',  ( 0.3581828924050323715, -0.1743168766271109560, 0.3019256869348722616 ) ) ;
#2038=ORIENTED_EDGE ( 'NONE', *, *, #1441, .F. ) ;
#2050=( LENGTH_UNIT ( ) NAMED_UNIT ( * ) SI_UNIT ( $, .METRE. ) );
#2055=( NAMED_UNIT ( * ) SI_UNIT ( $, .STERADIAN. ) SOLID_ANGLE_UNIT ( ) );
#2064=VERTEX_POINT ( 'NONE', #6615 ) ;
#2073=CARTESIAN_POINT ( 'NONE',  ( 0.01832242175888466190, -0.1844213691142429778, -0.2711239997950803393 ) ) ;
#2098=DIRECTION ( 'NONE',  ( 0.000000000000000000, -0.5000000000000005551, 0.8660254037844382635 ) ) ;
#2102=DIRECTION ( 'NONE',  ( 1.000000000000000000, 0.000000000000000000, -0.000000000000000000 ) ) ;
#2107=CIRCLE ( 'NONE', #3934, 0.2362204724409449064 ) ;
#2111=DIRECTION ( 'NONE',  ( 0.000000000000000000, 0.000000000000000000, 1.000000000000000000 ) ) ;
#2123=CARTESIAN_POINT ( 'NONE',  ( 0.3411151615605803600, 0.2304996462388439749, 0.2037536041052391000 ) ) ;
#2128=CARTESIAN_POINT ( 'NONE',  ( 0.3426022948973417304, -0.05819196463765255456, -0.3015401604570891458 ) ) ;
#2134=DIRECTION ( 'NONE',  ( 0.000000000000000000, 0.000000000000000000, 1.000000000000000000 ) ) ;
#2139=EDGE_LOOP ( 'NONE', ( #6526, #5681, #1655, #521, #7071, #2334, #1519 ) ) ;
#2143=CARTESIAN_POINT ( 'NONE',  ( 0.3391892065151631552, -0.1988903486381589925, -0.2460629921259842035 ) ) ;
#2145=CARTESIAN_POINT ( 'NONE',  ( 0.3585569128062319200, 0.3496569568119790028, 0.001755940978325809575 ) ) ;
#2153=CARTESIAN_POINT ( 'NONE',  ( 0.01832242175888482497, -0.3270109559553083245, 0.02415159075610082487 ) ) ;
#2166=CARTESIAN_POINT ( 'NONE',  ( 0.3505601438611540277, -0.1704774416898505729, -0.2952755905511810774 ) ) ;
#2170=VECTOR ( 'NONE', #5143, 39.37007874015748143 ) ;
#2174=CARTESIAN_POINT ( 'NONE',  ( 0.000000000000000000, 0.2557161625347750267, 0.1476377952755908163 ) ) ;
#2176=DIRECTION ( 'NONE',  ( 0.000000000000000000, 0.000000000000000000, -1.000000000000000000 ) ) ;
#2184=CARTESIAN_POINT ( 'NONE',  ( 0.3465694189146783510, 0.1966695024996976682, -0.2499096104736449331 ) ) ;
#2185=CARTESIAN_POINT ( 'NONE',  ( 0.3465694189147059956, -0.1966695024996656382, 0.2499096104736426016 ) ) ;
#2186=CIRCLE ( 'NONE', #3158, 0.2952755905511810774 ) ;
#2193=CARTESIAN_POINT ( 'NONE',  ( 0.0006233585804807679088, 0.2412158484082065346, -0.1727530760685158651 ) ) ;
#2200=ORIENTED_EDGE ( 'NONE', *, *, #6928, .T. ) ;
#2210=LINE ( 'NONE', #3933, #7365 ) ;
#2212=DIRECTION ( 'NONE',  ( 1.000000000000000000, 0.000000000000000000, 0.000000000000000000 ) ) ;
#2220=CIRCLE ( 'NONE', #5035, 0.4507874015748032370 ) ;
#2223=CARTESIAN_POINT ( 'NONE',  ( 0.3496875272944827695, 0.1667004943313749321, -0.3018174552735724547 ) ) ;
#2224=CARTESIAN_POINT ( 'NONE',  ( 0.3565325103478088065, -0.3440765519545064266, -0.005406888575953978406 ) ) ;
#2233=ORIENTED_EDGE ( 'NONE', *, *, #5280, .T. ) ;
#2234=CARTESIAN_POINT ( 'NONE',  ( 0.01171324505787542034, 0.1984117137466533121, -0.2468920120763460069 ) ) ;
#2235=EDGE_LOOP ( 'NONE', ( #1750, #3381, #3394, #5682 ) ) ;
#2260=CARTESIAN_POINT ( 'NONE',  ( 0.3531511627980760681, 0.1878266560944092389, -0.2783075040405467715 ) ) ;
#2265=CARTESIAN_POINT ( 'NONE',  ( 0.3391892065151631552, -0.3125419764313924209, 0.04921259842519686012 ) ) ;
#2274=CARTESIAN_POINT ( 'NONE',  ( 0.3391892065151630442, 0.3125419764313920878, -0.04921259842519681155 ) ) ;
#2281=ADVANCED_FACE ( 'NONE', ( #4015 ), #815, .F. ) ;
#2297=EDGE_LOOP ( 'NONE', ( #4287, #550, #1632 ) ) ;
#2309=DIRECTION ( 'NONE',  ( -0.000000000000000000, 0.000000000000000000, 1.000000000000000000 ) ) ;
#2321=CARTESIAN_POINT ( 'NONE',  ( 0.3410076799406686066, -0.2467857494855110190, 0.1755389823809323790 ) ) ;
#2334=ORIENTED_EDGE ( 'NONE', *, *, #4305, .T. ) ;
#2344=CARTESIAN_POINT ( 'NONE',  ( 0.3483227611829848303, 0.3409548833797004797, 0.000000000000000000 ) ) ;
#2347=CONICAL_SURFACE ( 'NONE', #6637, 0.2952755905511810774, 1.047197551196600518 ) ;
#2348=CARTESIAN_POINT ( 'NONE',  ( 0.3565422270302660013, -0.3441025489056189213, 0.005451916616122784963 ) ) ;
#2372=CARTESIAN_POINT ( 'NONE',  ( 0.3585568952266072751, -0.1763490727872195629, 0.3019338363380300039 ) ) ;
#2375=DIRECTION ( 'NONE',  ( 0.3420201433256623291, 1.150791560227853228E-16, 0.9396926207859106484 ) ) ;
#2376=FACE_OUTER_BOUND ( 'NONE', #3648, .T. ) ;
#2381=DIRECTION ( 'NONE',  ( 0.000000000000000000, 0.000000000000000000, -1.000000000000000000 ) ) ;
#2382=VERTEX_POINT ( 'NONE', #2968 ) ;
#2385=CARTESIAN_POINT ( 'NONE',  ( 0.3426144402833997127, -0.2904173629089126796, -0.1000635707556142007 ) ) ;
#2392=CARTESIAN_POINT ( 'NONE',  ( 0.02637295201093723881, -0.1704774416898505729, -0.2952755905511810774 ) ) ;
#2396=CARTESIAN_POINT ( 'NONE',  ( 0.01178921041716320811, 0.1149842948508782436, 0.2952755905511810774 ) ) ;
#2397=CARTESIAN_POINT ( 'NONE',  ( 0.000000000000000000, 0.2557161625347749712, -0.1476377952755909551 ) ) ;
#2413=CARTESIAN_POINT ( 'NONE',  ( 0.3487098613656773316, 0.1177053732609037312, 0.3017042368166658051 ) ) ;
#2426=CARTESIAN_POINT ( 'NONE',  ( 0.3496779274129793169, -0.1667266398149501727, -0.3017721699676331748 ) ) ;
#2431=EDGE_CURVE ( 'NONE', #4413, #5853, #193, .T. ) ;
#2434=CARTESIAN_POINT ( 'NONE',  ( 0.3574299024618896037, 0.1732824651941676231, 0.3001340337771135625 ) ) ;
#2438=CARTESIAN_POINT ( 'NONE',  ( 0.02637295201093697167, 0.1704774416898497680, -0.2952755905511810774 ) ) ;
#2439=DIRECTION ( 'NONE',  ( 0.000000000000000000, 0.5000000000000018874, 0.8660254037844375974 ) ) ;
#2443=VECTOR ( 'NONE', #2375, 39.37007874015748143 ) ;
#2452=PRODUCT ( 'hex flange bolt small_iso_ISO 4162 - M12 x 30 x 30-N', 'hex flange bolt small_iso_ISO 4162 - M12 x 30 x 30-N', '', ( #3063 ) ) ;
#2459=ORIENTED_EDGE ( 'NONE', *, *, #7472, .T. ) ;
#2473=VECTOR ( 'NONE', #474, 39.37007874015748143 ) ;
#2482=DIRECTION ( 'NONE',  ( 0.000000000000000000, -0.8660254037844381525, -0.5000000000000009992 ) ) ;
#2483=CARTESIAN_POINT ( 'NONE',  ( 0.3485777078273625817, 0.2029921329169074307, 0.2518088348849962799 ) ) ;
#2486=ORIENTED_EDGE ( 'NONE', *, *, #1439, .T. ) ;
#2487=AXIS2_PLACEMENT_3D ( 'NONE', #954, #2102, #6910 ) ;
#2492=EDGE_CURVE ( 'NONE', #3692, #1170, #952, .T. ) ;
#2496=EDGE_LOOP ( 'NONE', ( #6165, #1970, #483, #397 ) ) ;
#2506=CARTESIAN_POINT ( 'NONE',  ( 0.3409812221349221573, -0.2754857644942658168, -0.1258275564122679768 ) ) ;
#2524=CARTESIAN_POINT ( 'NONE',  ( 0.3487105584742864473, -0.1177098269287414900, -0.3017042544367490309 ) ) ;
#2526=FACE_OUTER_BOUND ( 'NONE', #2496, .T. ) ;
#2550=CARTESIAN_POINT ( 'NONE',  ( 0.3581828924050323715, 0.1743168766271109560, 0.3019256869348722616 ) ) ;
#2562=DIRECTION ( 'NONE',  ( -1.000000000000000000, -0.000000000000000000, -0.000000000000000000 ) ) ;
#2564=CARTESIAN_POINT ( 'NONE',  ( 0.3505602286436571013, -0.1704774416898497957, 0.2952755905511814660 ) ) ;
#2571=CARTESIAN_POINT ( 'NONE',  ( 0.3391216574609289269, 0.1954800165277119361, 0.2519698606119610829 ) ) ;
#2588=FACE_OUTER_BOUND ( 'NONE', #4055, .T. ) ;
#2593=ORIENTED_EDGE ( 'NONE', *, *, #6368, .T. ) ;
#2600=CARTESIAN_POINT ( 'NONE',  ( 0.000000000000000000, -0.2557161625347750822, -0.1476377952755907330 ) ) ;
#2607=CARTESIAN_POINT ( 'NONE',  ( 0.3527006543068526567, -0.3418446578861590868, 8.418741006566202135E-18 ) ) ;
#2616=ORIENTED_EDGE ( 'NONE', *, *, #3081, .T. ) ;
#2625=CARTESIAN_POINT ( 'NONE',  ( 0.3306743754077733910, -1.707404996040164512E-17, 0.2952755905511811885 ) ) ;
#2626=CARTESIAN_POINT ( 'NONE',  ( 0.3527006543068523237, 0.1709223289430787940, -0.2960461578774135072 ) ) ;
#2631=CARTESIAN_POINT ( 'NONE',  ( 0.3561392902752972267, 0.3446605091515489439, -2.917830865379561131E-17 ) ) ;
#2632=DIRECTION ( 'NONE',  ( 0.000000000000000000, 0.000000000000000000, 1.000000000000000000 ) ) ;
#2634=CARTESIAN_POINT ( 'NONE',  ( 0.3321025531238107620, -0.02909241602403181068, -0.2952755905511810774 ) ) ;
#2639=CARTESIAN_POINT ( 'NONE',  ( 0.3581828924050323715, -0.1743168766271109560, 0.3019256869348722616 ) ) ;
#2644=CARTESIAN_POINT ( 'NONE',  ( 0.3483227611829849413, -0.3409548833797009237, 0.000000000000000000 ) ) ;
#2648=ORIENTED_EDGE ( 'NONE', *, *, #5676, .F. ) ;
#2654=LENGTH_MEASURE_WITH_UNIT ( LENGTH_MEASURE( 0.02539999999999999897 ), #865 );
#2665=FACE_OUTER_BOUND ( 'NONE', #2685, .T. ) ;
#2668=FACE_OUTER_BOUND ( 'NONE', #5310, .T. ) ;
#2670=CARTESIAN_POINT ( 'NONE',  ( 1.649606299212598381, 0.000000000000000000, 0.000000000000000000 ) ) ;
#2671=CARTESIAN_POINT ( 'NONE',  ( 0.3337358785015786533, -0.05918271685993679171, -0.2952755905511810774 ) ) ;
#2674=EDGE_LOOP ( 'NONE', ( #887, #7384, #2616, #5981, #4968 ) ) ;
#2684=CARTESIAN_POINT ( 'NONE',  ( 0.3496779274129791504, 0.1667266398149495066, 0.3017721699676332303 ) ) ;
#2685=EDGE_LOOP ( 'NONE', ( #6897, #6812, #4628, #1207 ) ) ;
#2708=AXIS2_PLACEMENT_3D ( 'NONE', #1145, #6437, #4608 ) ;
#2720=CARTESIAN_POINT ( 'NONE',  ( 0.3510872220068100846, -0.1819230426404178091, 0.2754512281816298147 ) ) ;
#2728=ORIENTED_EDGE ( 'NONE', *, *, #3748, .T. ) ;
#2737=CARTESIAN_POINT ( 'NONE',  ( 0.4685039370078740717, 2.892866454678787531E-17, -0.2362204724409449064 ) ) ;
#2741=DIRECTION ( 'NONE',  ( 1.000000000000000000, 0.000000000000000000, 0.000000000000000000 ) ) ;
#2742=CARTESIAN_POINT ( 'NONE',  ( 0.3574269917172681610, 0.1732784665916975442, -0.3001271079942677833 ) ) ;
#2750=B_SPLINE_CURVE_WITH_KNOTS ( 'NONE', 3,
 ( #2344, #6976, #2274, #55, #1182, #593, #5294, #3463, #5832 ),
 .UNSPECIFIED., .F., .F.,
 ( 4, 2, 1, 2, 4 ),
 ( 2.312923578716022130E-20, 0.002165063509461098365, 0.004330127018922196730, 0.006495190528383295095, 0.008660254037844393460 ),
 .UNSPECIFIED. ) ;
#2752=CARTESIAN_POINT ( 'NONE',  ( 0.3337354549120237213, 0.2261274626982069103, -0.1988869267224314119 ) ) ;
#2762=VERTEX_POINT ( 'NONE', #5825 ) ;
#2764=EDGE_CURVE ( 'NONE', #4703, #7025, #499, .T. ) ;
#2779=DIRECTION ( 'NONE',  ( 0.000000000000000000, 0.000000000000000000, 1.000000000000000000 ) ) ;
#2791=CARTESIAN_POINT ( 'NONE',  ( 0.3585665126877354281, -0.1732820025503174766, 0.3037348580927970443 ) ) ;
#2798=CARTESIAN_POINT ( 'NONE',  ( -6.322734125961233610E-17, -0.2702383257424528229, 0.1224846707640861176 ) ) ;
#2800=CARTESIAN_POINT ( 'NONE',  ( 0.3336175750056032951, -0.2273032555864670234, 0.1968503937007874682 ) ) ;
#2801=ORIENTED_EDGE ( 'NONE', *, *, #6403, .F. ) ;
#2809=DIRECTION ( 'NONE',  ( -1.000000000000000000, -0.000000000000000000, -0.000000000000000000 ) ) ;
#2814=DIRECTION ( 'NONE',  ( 0.000000000000000000, 0.000000000000000000, 1.000000000000000000 ) ) ;
#2823=CARTESIAN_POINT ( 'NONE',  ( 0.3459463601587655091, 0.3157502742998894996, -0.04365566351111115767 ) ) ;
#2824=DIRECTION ( 'NONE',  ( 0.000000000000000000, 0.000000000000000000, 1.000000000000000000 ) ) ;
#2827=ORIENTED_EDGE ( 'NONE', *, *, #3748, .F. ) ;
#2830=B_SPLINE_CURVE_WITH_KNOTS ( 'NONE', 3,
 ( #3577, #142, #7131, #6034, #3036, #5335, #746, #2998 ),
 .UNSPECIFIED., .F., .F.,
 ( 4, 2, 2, 4 ),
 ( 0.004381617662950684777, 0.005472867551409519790, 0.006564117439868355670, 0.008746617216786024829 ),
 .UNSPECIFIED. ) ;
#2862=CARTESIAN_POINT ( 'NONE',  ( 0.3409812221349244332, -0.2467127425962881426, 0.1756638922268692060 ) ) ;
#2865=ORIENTED_EDGE ( 'NONE', *, *, #4460, .T. ) ;
#2867=CARTESIAN_POINT ( 'NONE',  ( 0.000000000000000000, -0.2557161625347748601, 0.1476377952755911216 ) ) ;
#2880=CARTESIAN_POINT ( 'NONE',  ( 0.000000000000000000, 0.000000000000000000, 0.000000000000000000 ) ) ;
#2893=B_SPLINE_CURVE_WITH_KNOTS ( 'NONE', 3,
 ( #4857, #2073, #7184, #6625, #279, #2600 ),
 .UNSPECIFIED., .F., .F.,
 ( 4, 2, 4 ),
 ( 2.380732026385019675E-07, 0.002190927868076661400, 0.004381617662950684777 ),
 .UNSPECIFIED. ) ;
#2894=ORIENTED_EDGE ( 'NONE', *, *, #7103, .F. ) ;
#2907=CARTESIAN_POINT ( 'NONE',  ( 0.3479985092864859020, -0.1192235226163089606, 0.3017044423212984494 ) ) ;
#2923=CIRCLE ( 'NONE', #7090, 0.4629062255509093782 ) ;
#2926=CARTESIAN_POINT ( 'NONE',  ( 0.3410249605999031153, 0.02920150297965299485, -0.3014927230551893711 ) ) ;
#2928=EDGE_CURVE ( 'NONE', #5498, #5789, #1818, .T. ) ;
#2938=DIRECTION ( 'NONE',  ( 1.000000000000000000, 0.000000000000000000, 0.000000000000000000 ) ) ;
#2953=CARTESIAN_POINT ( 'NONE',  ( 0.000000000000000000, 0.000000000000000000, 0.000000000000000000 ) ) ;
#2968=CARTESIAN_POINT ( 'NONE',  ( 0.3581828924050324825, -0.1743168766271116221, -0.3019256869348722061 ) ) ;
#2981=CARTESIAN_POINT ( 'NONE',  ( 0.000000000000000000, 0.000000000000000000, 0.000000000000000000 ) ) ;
#2985=FACE_OUTER_BOUND ( 'NONE', #4226, .T. ) ;
#2998=CARTESIAN_POINT ( 'NONE',  ( 0.02637295201093751290, -0.3409548833797009237, -9.138209691400258722E-18 ) ) ;
#3014=ORIENTED_EDGE ( 'NONE', *, *, #3081, .F. ) ;
#3027=CONICAL_SURFACE ( 'NONE', #4994, 0.2952755905511810774, 1.047197551196600518 ) ;
#3029=B_SPLINE_CURVE_WITH_KNOTS ( 'NONE', 3,
 ( #7361, #2742, #6799, #2626, #1548, #3895 ),
 .UNSPECIFIED., .F., .F.,
 ( 4, 2, 4 ),
 ( -3.269571951033989319E-06, 0.0001651384380483822119, 0.0003335464480477984012 ),
 .UNSPECIFIED. ) ;
#3033=VECTOR ( 'NONE', #7110, 39.37007874015748143 ) ;
#3036=CARTESIAN_POINT ( 'NONE',  ( 0.004822332172886453772, -0.2917300191221102734, -0.08525996588982823199 ) ) ;
#3040=CIRCLE ( 'NONE', #3536, 0.2952755905511810774 ) ;
#3046=CARTESIAN_POINT ( 'NONE',  ( 0.4685039370078740717, 0.3409548833797004797, 0.000000000000000000 ) ) ;
#3048=ORIENTED_EDGE ( 'NONE', *, *, #339, .F. ) ;
#3050=CARTESIAN_POINT ( 'NONE',  ( 0.3528822938286762523, 0.1453909600788098055, -0.3018098512751524187 ) ) ;
#3051=CARTESIAN_POINT ( 'NONE',  ( 0.3410425348215776475, -0.2759054741781712949, 0.1251041708914593653 ) ) ;
#3055=ORIENTED_EDGE ( 'NONE', *, *, #3739, .F. ) ;
#3063=PRODUCT_CONTEXT ( 'NONE', #3652, 'mechanical' ) ;
#3064=AXIS2_PLACEMENT_3D ( 'NONE', #107, #6536, #1277 ) ;
#3074=LENGTH_MEASURE_WITH_UNIT ( LENGTH_MEASURE( 0.02539999999999999897 ), #2050 );
#3081=EDGE_CURVE ( 'NONE', #4759, #6192, #3742, .T. ) ;
#3088=EDGE_CURVE ( 'NONE', #210, #6925, #4124, .T. ) ;
#3089=CARTESIAN_POINT ( 'NONE',  ( 0.3581828924050324825, 0.3486337532542225226, 1.056976728655274672E-17 ) ) ;
#3097=AXIS2_PLACEMENT_3D ( 'NONE', #2880, #6406, #3498 ) ;
#3102=AXIS2_PLACEMENT_3D ( 'NONE', #5053, #3209, #4475 ) ;
#3107=CARTESIAN_POINT ( 'NONE',  ( 0.3565325103478085289, 0.1673557731150444039, 0.3006824791271354158 ) ) ;
#3111=ORIENTED_EDGE ( 'NONE', *, *, #3794, .T. ) ;
#3112=CARTESIAN_POINT ( 'NONE',  ( 0.3322361761492684806, -0.2247851515112275766, -0.2012118778978489453 ) ) ;
#3121=CARTESIAN_POINT ( 'NONE',  ( -2.614463900186501485E-17, 0.02884736746568806673, -0.2952755905511810774 ) ) ;
#3132=ADVANCED_FACE ( 'NONE', ( #7108 ), #1867, .F. ) ;
#3134=FACE_OUTER_BOUND ( 'NONE', #1759, .T. ) ;
#3151=ORIENTED_EDGE ( 'NONE', *, *, #7198, .T. ) ;
#3152=CARTESIAN_POINT ( 'NONE',  ( 1.611653543307086212, 0.000000000000000000, 0.000000000000000000 ) ) ;
#3158=AXIS2_PLACEMENT_3D ( 'NONE', #3670, #4161, #3745 ) ;
#3161=CARTESIAN_POINT ( 'NONE',  ( 0.000000000000000000, 0.2557161625347750267, 0.1476377952755908163 ) ) ;
#3170=DIRECTION ( 'NONE',  ( 0.000000000000000000, 0.000000000000000000, 1.000000000000000000 ) ) ;
#3172=ORIENTED_EDGE ( 'NONE', *, *, #3887, .F. ) ;
#3187=ORIENTED_EDGE ( 'NONE', *, *, #4305, .F. ) ;
#3188=AXIS2_PLACEMENT_3D ( 'NONE', #3152, #3693, #708 ) ;
#3204=CARTESIAN_POINT ( 'NONE',  ( 0.3483227611829846637, -0.1704774416898499345, 0.2952755905511811330 ) ) ;
#3209=DIRECTION ( 'NONE',  ( -0.000000000000000000, 1.000000000000000000, 1.224646799147353207E-16 ) ) ;
#3215=( BOUNDED_SURFACE ( )  B_SPLINE_SURFACE ( 3, 2, ( 
 ( #4623, #2224, #4016 ),
 ( #5784, #393, #6922 ),
 ( #5679, #6240, #437 ),
 ( #1679, #3368, #2862 ),
 ( #5095, #7412, #6891 ),
 ( #5205, #2185, #3988 ),
 ( #4519, #2720, #1037 ),
 ( #6348, #1605, #2791 ) ),
 .UNSPECIFIED., .F., .F., .F. ) 
 B_SPLINE_SURFACE_WITH_KNOTS ( ( 4, 2, 2, 4 ),
 ( 3, 3 ),
 ( 0.03551798592901338203, 0.03994769179990646790, 0.04216254473535301084, 0.04437739767079956071 ),
 ( 0.000000000000000000, 1.000000000000000000 ),
 .UNSPECIFIED. ) 
 GEOMETRIC_REPRESENTATION_ITEM ( )  RATIONAL_B_SPLINE_SURFACE ( (
 ( 1.000000000000000000, 0.8047781103519389134, 1.000000000000000000),
 ( 1.000000000000000000, 0.8123785826170312196, 1.000000000000000000),
 ( 1.000000000000000000, 0.8190671539034724002, 1.000000000000000000),
 ( 1.000000000000000000, 0.8191932076449992550, 1.000000000000000000),
 ( 1.000000000000000000, 0.8176085094069774906, 1.000000000000000000),
 ( 1.000000000000000000, 0.8122955484010631055, 1.000000000000000000),
 ( 1.000000000000000000, 0.8086308001283356583, 1.000000000000000000),
 ( 1.000000000000000000, 0.8047712537969732294, 1.000000000000000000) ) ) 
 REPRESENTATION_ITEM ( '' )  SURFACE ( )  );
#3223=EDGE_LOOP ( 'NONE', ( #258, #2827 ) ) ;
#3230=ORIENTED_EDGE ( 'NONE', *, *, #1115, .T. ) ;
#3241=DIRECTION ( 'NONE',  ( 0.000000000000000000, 0.000000000000000000, -1.000000000000000000 ) ) ;
#3243=DIRECTION ( 'NONE',  ( 1.000000000000000000, 0.000000000000000000, 0.000000000000000000 ) ) ;
#3245=CARTESIAN_POINT ( 'NONE',  ( 0.3388530074223801147, 0.06137376066181338130, -0.2952755905511810774 ) ) ;
#3284=CARTESIAN_POINT ( 'NONE',  ( 0.3426404862726872280, -0.2318193597401798645, -0.2015595396344879719 ) ) ;
#3290=LINE ( 'NONE', #962, #2473 ) ;
#3293=CARTESIAN_POINT ( 'NONE',  ( 0.01165389088406399223, -0.1143408654217484000, -0.2952755905511810219 ) ) ;
#3298=EDGE_LOOP ( 'NONE', ( #6286, #6214, #2593 ) ) ;
#3300=ORIENTED_EDGE ( 'NONE', *, *, #4904, .F. ) ;
#3309=CARTESIAN_POINT ( 'NONE',  ( 0.000000000000000000, 2.957312202238506242E-17, 0.2952755905511810774 ) ) ;
#3320=CARTESIAN_POINT ( 'NONE',  ( 0.002479217192759452203, -0.05744896992506681732, 0.2952755905511810774 ) ) ;
#3327=ADVANCED_FACE ( 'NONE', ( #2985 ), #3964, .F. ) ;
#3332=CARTESIAN_POINT ( 'NONE',  ( 0.3409812221349237671, 0.2467127425963012433, -0.1756638922268426994 ) ) ;
#3339=ORIENTED_EDGE ( 'NONE', *, *, #1439, .F. ) ;
#3345=VECTOR ( 'NONE', #4542, 39.37007874015748143 ) ;
#3354=DIMENSIONAL_EXPONENTS ( 1.000000000000000000, 0.000000000000000000, 0.000000000000000000, 0.000000000000000000, 0.000000000000000000, 0.000000000000000000, 0.000000000000000000 ) ;
#3357=CARTESIAN_POINT ( 'NONE',  ( 0.000000000000000000, 0.000000000000000000, 0.000000000000000000 ) ) ;
#3360=PLANE ( 'NONE',  #2487 ) ;
#3363=CARTESIAN_POINT ( 'NONE',  ( 0.3997746709170348356, 0.000000000000000000, 0.000000000000000000 ) ) ;
#3368=CARTESIAN_POINT ( 'NONE',  ( 0.3387177083556423551, -0.2412911239081454440, 0.1726226950780508362 ) ) ;
#3379=ORIENTED_EDGE ( 'NONE', *, *, #4067, .T. ) ;
#3381=ORIENTED_EDGE ( 'NONE', *, *, #4662, .F. ) ;
#3390=CARTESIAN_POINT ( 'NONE',  ( 1.649606299212598381, 0.000000000000000000, 0.000000000000000000 ) ) ;
#3394=ORIENTED_EDGE ( 'NONE', *, *, #6928, .F. ) ;
#3398=CARTESIAN_POINT ( 'NONE',  ( 0.3565422129079688918, -0.1767726971815447856, -0.2952755905511810774 ) ) ;
#3403=EDGE_CURVE ( 'NONE', #2382, #1950, #6872, .T. ) ;
#3404=CARTESIAN_POINT ( 'NONE',  ( 0.3432736861146661878, -0.3267484299055466446, -0.02460629921259840577 ) ) ;
#3414=CARTESIAN_POINT ( 'NONE',  ( 0.3336175750056032396, 0.05682581389661631177, -0.2952755905511810219 ) ) ;
#3435=FACE_OUTER_BOUND ( 'NONE', #5895, .T. ) ;
#3455=AXIS2_PLACEMENT_3D ( 'NONE', #5554, #1366, #3747 ) ;
#3456=EDGE_CURVE ( 'NONE', #6629, #7446, #6955, .T. ) ;
#3463=CARTESIAN_POINT ( 'NONE',  ( 0.3432736861146659102, 0.1846838951640040472, -0.2706692913385826404 ) ) ;
#3471=B_SPLINE_CURVE_WITH_KNOTS ( 'NONE', 3,
 ( #1634, #4476, #4045, #509, #6310, #6378, #3284, #385, #7101, #606 ),
 .UNSPECIFIED., .F., .F.,
 ( 4, 2, 2, 2, 4 ),
 ( 6.564673817405236669E-19, 0.002239656411828510989, 0.004479312823657021110, 0.006718969235485531231, 0.008958625647314040485 ),
 .UNSPECIFIED. ) ;
#3483=DIRECTION ( 'NONE',  ( 0.000000000000000000, 0.000000000000000000, -1.000000000000000000 ) ) ;
#3498=DIRECTION ( 'NONE',  ( 0.000000000000000000, 0.000000000000000000, -1.000000000000000000 ) ) ;
#3515=ORIENTED_EDGE ( 'NONE', *, *, #7250, .F. ) ;
#3525=CARTESIAN_POINT ( 'NONE',  ( 0.3465690653189043013, 0.1180910924887165481, 0.2952755905511810774 ) ) ;
#3528=DIRECTION ( 'NONE',  ( 1.000000000000000000, 0.000000000000000000, 0.000000000000000000 ) ) ;
#3536=AXIS2_PLACEMENT_3D ( 'NONE', #6904, #5192, #4534 ) ;
#3544=FACE_OUTER_BOUND ( 'NONE', #3603, .T. ) ;
#3563=DIRECTION ( 'NONE',  ( 1.000000000000000000, 0.000000000000000000, -0.000000000000000000 ) ) ;
#3567=CARTESIAN_POINT ( 'NONE',  ( 0.3398308759505395682, 0.1188917464549260616, 0.2952755905511810774 ) ) ;
#3577=CARTESIAN_POINT ( 'NONE',  ( 0.000000000000000000, -0.2557161625347750822, -0.1476377952755907330 ) ) ;
#3582=CIRCLE ( 'NONE', #3097, 0.2952755905511810774 ) ;
#3587=CARTESIAN_POINT ( 'NONE',  ( 0.4685039370078740717, -0.1704774416898499345, 0.2952755905511811330 ) ) ;
#3588=CARTESIAN_POINT ( 'NONE',  ( 0.3410249605999788325, 0.02903799983316233957, 0.3014927230551917026 ) ) ;
#3603=EDGE_LOOP ( 'NONE', ( #1553, #3339 ) ) ;
#3615=CARTESIAN_POINT ( 'NONE',  ( 0.3337354549119980751, -0.2853048623713481113, -0.09638866382874244909 ) ) ;
#3618=FACE_OUTER_BOUND ( 'NONE', #4977, .T. ) ;
#3638=ORIENTED_EDGE ( 'NONE', *, *, #2764, .T. ) ;
#3643=CARTESIAN_POINT ( 'NONE',  ( 0.3565324925542818213, -0.1767206836160838956, 0.2952755905511811885 ) ) ;
#3648=EDGE_LOOP ( 'NONE', ( #293, #315, #2002 ) ) ;
#3652=APPLICATION_CONTEXT ( 'automotive_design' ) ;
#3659=CARTESIAN_POINT ( 'NONE',  ( 0.3531511627980769008, -0.3349346966101605649, -0.02350890366535178522 ) ) ;
#3661=VECTOR ( 'NONE', #3702, 39.37007874015748143 ) ;
#3670=CARTESIAN_POINT ( 'NONE',  ( 0.000000000000000000, 0.000000000000000000, 0.000000000000000000 ) ) ;
#3678=LINE ( 'NONE', #3788, #753 ) ;
#3679=CARTESIAN_POINT ( 'NONE',  ( 0.3581828924050323715, 0.1743168766271109560, 0.3019256869348722616 ) ) ;
#3692=VERTEX_POINT ( 'NONE', #3309 ) ;
#3693=DIRECTION ( 'NONE',  ( -1.000000000000000000, -0.000000000000000000, -0.000000000000000000 ) ) ;
#3702=DIRECTION ( 'NONE',  ( -1.000000000000000000, -0.000000000000000000, -0.000000000000000000 ) ) ;
#3703=EDGE_CURVE ( 'NONE', #5110, #5853, #6842, .T. ) ;
#3713=DIRECTION ( 'NONE',  ( -1.000000000000000000, -0.000000000000000000, -0.000000000000000000 ) ) ;
#3716=LINE ( 'NONE', #1995, #45 ) ;
#3717=CARTESIAN_POINT ( 'NONE',  ( 0.3398315730591770500, -0.1188962366173021562, -0.2952755905511810774 ) ) ;
#3729=CARTESIAN_POINT ( 'NONE',  ( 0.3459463601587901560, 0.1956820507697113742, 0.2516199270399913090 ) ) ;
#3737=B_SPLINE_CURVE_WITH_KNOTS ( 'NONE', 3,
 ( #5453, #5568, #4292, #2607, #1339, #2644 ),
 .UNSPECIFIED., .F., .F.,
 ( 4, 2, 4 ),
 ( -3.269571951034336179E-06, 0.0001651384380483830793, 0.0003335464480478004612 ),
 .UNSPECIFIED. ) ;
#3739=EDGE_CURVE ( 'NONE', #7262, #6925, #3040, .T. ) ;
#3742=LINE ( 'NONE', #3587, #5136 ) ;
#3745=DIRECTION ( 'NONE',  ( 0.000000000000000000, 0.000000000000000000, 1.000000000000000000 ) ) ;
#3746=ORIENTED_EDGE ( 'NONE', *, *, #4026, .T. ) ;
#3747=DIRECTION ( 'NONE',  ( 0.000000000000000000, 0.000000000000000000, 1.000000000000000000 ) ) ;
#3748=EDGE_CURVE ( 'NONE', #4293, #6087, #4395, .T. ) ;
#3755=DIRECTION ( 'NONE',  ( 0.000000000000000000, 0.000000000000000000, 1.000000000000000000 ) ) ;
#3761=VERTEX_POINT ( 'NONE', #2737 ) ;
#3777=DIRECTION ( 'NONE',  ( -1.000000000000000000, -0.000000000000000000, 0.000000000000000000 ) ) ;
#3780=CARTESIAN_POINT ( 'NONE',  ( 0.3425764178929368575, 0.2900721174007582781, 0.1006592143205869566 ) ) ;
#3784=CARTESIAN_POINT ( 'NONE',  ( 0.3483227611829848303, 0.3409548833797004797, 0.000000000000000000 ) ) ;
#3788=CARTESIAN_POINT ( 'NONE',  ( 0.3997746709170348356, 0.000000000000000000, -0.4629062255509093782 ) ) ;
#3790=CARTESIAN_POINT ( 'NONE',  ( 1.649606299212598381, 0.000000000000000000, 0.000000000000000000 ) ) ;
#3792=CARTESIAN_POINT ( 'NONE',  ( 0.3483227611829849413, -0.3409548833797009237, 0.000000000000000000 ) ) ;
#3794=EDGE_CURVE ( 'NONE', #2762, #6349, #1015, .T. ) ;
#3809=DIRECTION ( 'NONE',  ( 0.000000000000000000, 0.000000000000000000, 1.000000000000000000 ) ) ;
#3837=CONICAL_SURFACE ( 'NONE', #5794, 0.4629062255509093782, 1.221730476396037490 ) ;
#3843=VERTEX_POINT ( 'NONE', #5156 ) ;
#3857=CARTESIAN_POINT ( 'NONE',  ( 0.4685039370078740717, 0.000000000000000000, 0.2362204724409449064 ) ) ;
#3863=DIRECTION ( 'NONE',  ( 1.000000000000000000, 0.000000000000000000, -0.000000000000000000 ) ) ;
#3887=EDGE_CURVE ( 'NONE', #1388, #7025, #556, .T. ) ;
#3895=CARTESIAN_POINT ( 'NONE',  ( 0.3483227611829846082, 0.1704774416898497680, -0.2952755905511810774 ) ) ;
#3900=CARTESIAN_POINT ( 'NONE',  ( 0.01836325778988323956, -0.1427310470019406141, 0.2952755905511810774 ) ) ;
#3908=CARTESIAN_POINT ( 'NONE',  ( 0.3411151615605715337, 0.2917056203871458142, -0.09774174715358552312 ) ) ;
#3915=AXIS2_PLACEMENT_3D ( 'NONE', #5731, #6975, #4574 ) ;
#3933=CARTESIAN_POINT ( 'NONE',  ( 0.4685039370078740717, -0.1704774416898505729, -0.2952755905511810774 ) ) ;
#3934=AXIS2_PLACEMENT_3D ( 'NONE', #1318, #3777, #868 ) ;
#3945=DIRECTION ( 'NONE',  ( -1.000000000000000000, -0.000000000000000000, -0.000000000000000000 ) ) ;
#3950=CARTESIAN_POINT ( 'NONE',  ( 0.3585665126877354281, 0.1732820025503171713, -0.3037348580927971553 ) ) ;
#3961=ORIENTED_EDGE ( 'NONE', *, *, #4067, .F. ) ;
#3964=( BOUNDED_SURFACE ( )  B_SPLINE_SURFACE ( 3, 2, ( 
 ( #1298, #3643, #2372 ),
 ( #5986, #738, #2907 ),
 ( #4136, #4097, #588 ),
 ( #12, #7004, #1842 ),
 ( #85, #1176, #1263 ),
 ( #3567, #3525, #2413 ),
 ( #1218, #5864, #4706 ),
 ( #7039, #1794, #4749 ) ),
 .UNSPECIFIED., .F., .F., .F. ) 
 B_SPLINE_SURFACE_WITH_KNOTS ( ( 4, 2, 2, 4 ),
 ( 3, 3 ),
 ( 0.03551233549299846748, 0.03994185813602711688, 0.04215661945754144158, 0.04437138077905577321 ),
 ( 0.000000000000000000, 1.000000000000000000 ),
 .UNSPECIFIED. ) 
 GEOMETRIC_REPRESENTATION_ITEM ( )  RATIONAL_B_SPLINE_SURFACE ( (
 ( 1.000000000000000000, 0.8047781229087798138, 1.000000000000000000),
 ( 1.000000000000000000, 0.8123782171506571670, 1.000000000000000000),
 ( 1.000000000000000000, 0.8190665209243362943, 1.000000000000000000),
 ( 1.000000000000000000, 0.8191935049886309717, 1.000000000000000000),
 ( 1.000000000000000000, 0.8176088963536531917, 1.000000000000000000),
 ( 1.000000000000000000, 0.8122958360081882212, 1.000000000000000000),
 ( 1.000000000000000000, 0.8086309270602213273, 1.000000000000000000),
 ( 1.000000000000000000, 0.8047712437947333042, 1.000000000000000000) ) ) 
 REPRESENTATION_ITEM ( '' )  SURFACE ( )  );
#3965=CARTESIAN_POINT ( 'NONE',  ( 0.3485616995351332181, -0.1165012447190267864, -0.3017003685801735724 ) ) ;
#3969=CARTESIAN_POINT ( 'NONE',  ( 0.0006233585804809438748, -0.2412158484082067011, 0.1727530760685163091 ) ) ;
#3975=PLANE ( 'NONE',  #5344 ) ;
#3988=CARTESIAN_POINT ( 'NONE',  ( 0.3487102105009278197, -0.2024297391849458061, 0.2527898980517221394 ) ) ;
#3995=DIRECTION ( 'NONE',  ( 1.000000000000000000, 0.000000000000000000, -0.000000000000000000 ) ) ;
#4008=CARTESIAN_POINT ( 'NONE',  ( 0.000000000000000000, 2.957312202238506242E-17, 0.2952755905511810774 ) ) ;
#4010=CARTESIAN_POINT ( 'NONE',  ( 0.3485534891173986405, -0.1164145375797935450, 0.3017001449125945034 ) ) ;
#4015=FACE_OUTER_BOUND ( 'NONE', #6516, .T. ) ;
#4016=CARTESIAN_POINT ( 'NONE',  ( 0.3585569128062321420, -0.3496569568119795024, -0.001755940978325754281 ) ) ;
#4023=CARTESIAN_POINT ( 'NONE',  ( 0.003035684155427062578, 0.2268414356900468054, -0.1976502892253328703 ) ) ;
#4026=EDGE_CURVE ( 'NONE', #6209, #5498, #3737, .T. ) ;
#4045=CARTESIAN_POINT ( 'NONE',  ( 0.3485373078438445127, -0.3194486952732369378, -0.05009812457233156491 ) ) ;
#4047=AXIS2_PLACEMENT_3D ( 'NONE', #6016, #6624, #2111 ) ;
#4052=CONICAL_SURFACE ( 'NONE', #4301, 0.2952755905511810774, 1.047197551196600518 ) ;
#4055=EDGE_LOOP ( 'NONE', ( #3172, #4717, #1452, #2008, #4946, #3230, #3638 ) ) ;
#4067=EDGE_CURVE ( 'NONE', #3843, #1950, #5014, .T. ) ;
#4069=DIRECTION ( 'NONE',  ( -1.000000000000000000, -0.000000000000000000, -0.000000000000000000 ) ) ;
#4095=ORIENTED_EDGE ( 'NONE', *, *, #3739, .T. ) ;
#4097=CARTESIAN_POINT ( 'NONE',  ( 0.3388543739203577765, -0.06138491293039709945, 0.2952755905511811330 ) ) ;
#4104=DIRECTION ( 'NONE',  ( 1.000000000000000000, 0.000000000000000000, 0.000000000000000000 ) ) ;
#4105=EDGE_CURVE ( 'NONE', #5789, #725, #5375, .T. ) ;
#4112=EDGE_CURVE ( 'NONE', #3843, #210, #6206, .T. ) ;
#4124=B_SPLINE_CURVE_WITH_KNOTS ( 'NONE', 3,
 ( #2438, #6080, #6612, #6006, #3121, #722 ),
 .UNSPECIFIED., .F., .F.,
 ( 4, 2, 4 ),
 ( 0.02186578511398849095, 0.02405896738650913774, 0.02625214965902978106 ),
 .UNSPECIFIED. ) ;
#4127=DIRECTION ( 'NONE',  ( 0.000000000000000000, -1.000000000000000000, 0.000000000000000000 ) ) ;
#4130=DIRECTION ( 'NONE',  ( 0.000000000000000000, 0.000000000000000000, -1.000000000000000000 ) ) ;
#4136=CARTESIAN_POINT ( 'NONE',  ( 0.3322368487464851805, -0.06186759433717738121, 0.2952755905511811330 ) ) ;
#4141=B_SPLINE_CURVE_WITH_KNOTS ( 'NONE', 3,
 ( #1945, #159, #6577, #5437, #194, #687 ),
 .UNSPECIFIED., .F., .F.,
 ( 4, 2, 4 ),
 ( 2.380732026380572752E-07, 0.002190927868076664002, 0.004381617662950689981 ),
 .UNSPECIFIED. ) ;
#4152=CARTESIAN_POINT ( 'NONE',  ( 0.4685039370078740717, -0.3409548833797009237, 0.000000000000000000 ) ) ;
#4159=CARTESIAN_POINT ( 'NONE',  ( 0.3581828924050324825, 0.3486337532542225226, 1.056976728655274672E-17 ) ) ;
#4160=CARTESIAN_POINT ( 'NONE',  ( 0.002549129251874865387, 0.05807386165059042621, 0.2952755905511811330 ) ) ;
#4161=DIRECTION ( 'NONE',  ( -1.000000000000000000, -0.000000000000000000, -0.000000000000000000 ) ) ;
#4163=CARTESIAN_POINT ( 'NONE',  ( 0.3581828924050323715, 0.1743168766271107895, -0.3019256869348722061 ) ) ;
#4190=CARTESIAN_POINT ( 'NONE',  ( 0.3388536909603144798, -0.2250264928541644005, -0.2007938624299156205 ) ) ;
#4204=CLOSED_SHELL ( 'NONE', ( #1111, #204, #4446, #4399, #6444, #4851, #39, #7329, #1345, #5835, #5993, #1685, #5326, #6448, #5845, #5892, #4811, #1397, #4776, #4547, #852, #3132, #6037, #5585, #7006, #3327, #7143, #1801, #2281 ) ) ;
#4207=EDGE_CURVE ( 'NONE', #6087, #7025, #4980, .T. ) ;
#4224=ORIENTED_EDGE ( 'NONE', *, *, #1483, .F. ) ;
#4226=EDGE_LOOP ( 'NONE', ( #990, #354, #5447, #3048, #5561 ) ) ;
#4245=FACE_OUTER_BOUND ( 'NONE', #4555, .T. ) ;
#4265=ORIENTED_EDGE ( 'NONE', *, *, #4105, .T. ) ;
#4287=ORIENTED_EDGE ( 'NONE', *, *, #1919, .T. ) ;
#4292=CARTESIAN_POINT ( 'NONE',  ( 0.3561390657006787142, -0.3446602609999988021, 5.012419073868498717E-17 ) ) ;
#4293=VERTEX_POINT ( 'NONE', #1135 ) ;
#4294=CARTESIAN_POINT ( 'NONE',  ( 0.3487102105009254327, 0.3201373431253348167, 0.04891434758976444946 ) ) ;
#4301=AXIS2_PLACEMENT_3D ( 'NONE', #2953, #4104, #2381 ) ;
#4302=AXIS2_PLACEMENT_3D ( 'NONE', #2981, #2938, #7150 ) ;
#4304=VERTEX_POINT ( 'NONE', #6422 ) ;
#4305=EDGE_CURVE ( 'NONE', #733, #4592, #2005, .T. ) ;
#4312=EDGE_CURVE ( 'NONE', #7325, #7262, #2893, .T. ) ;
#4315=CARTESIAN_POINT ( 'NONE',  ( 0.3432736861146659657, 0.1420645347415416815, 0.2952755905511811330 ) ) ;
#4319=CARTESIAN_POINT ( 'NONE',  ( 0.3410425348215775920, 0.2462961272004790259, 0.1763890642357578975 ) ) ;
#4338=CARTESIAN_POINT ( 'NONE',  ( 0.3496875272944829360, 0.3447318307381752600, -0.006541864722391422388 ) ) ;
#4367=ORIENTED_EDGE ( 'NONE', *, *, #7340, .T. ) ;
#4389=AXIS2_PLACEMENT_3D ( 'NONE', #3046, #2482, #4815 ) ;
#4395=CIRCLE ( 'NONE', #3915, 0.4507874015748032370 ) ;
#4399=ADVANCED_FACE ( 'NONE', ( #1916 ), #4940, .T. ) ;
#4400=CARTESIAN_POINT ( 'NONE',  ( 0.3997746709170348356, 5.668966274263039413E-17, 0.4629062255509093782 ) ) ;
#4407=ORIENTED_EDGE ( 'NONE', *, *, #4112, .F. ) ;
#4413=VERTEX_POINT ( 'NONE', #205 ) ;
#4415=CARTESIAN_POINT ( 'NONE',  ( 0.000000000000000000, 0.000000000000000000, 0.000000000000000000 ) ) ;
#4421=CARTESIAN_POINT ( 'NONE',  ( 0.3574269917172684941, -0.1732784665916271005, -0.3001271079943088615 ) ) ;
#4431=DIRECTION ( 'NONE',  ( -0.000000000000000000, 0.8660254037844383745, 0.5000000000000006661 ) ) ;
#4446=ADVANCED_FACE ( 'NONE', ( #2526 ), #5967, .T. ) ;
#4449=VERTEX_POINT ( 'NONE', #3679 ) ;
#4452=CARTESIAN_POINT ( 'NONE',  ( -1.320571051624814422E-17, -0.02882762270237488114, -0.2952755905511810219 ) ) ;
#4457=CARTESIAN_POINT ( 'NONE',  ( 0.3426144402834028768, 0.2904173629089201736, 0.1000635707556194326 ) ) ;
#4460=EDGE_CURVE ( 'NONE', #1950, #5498, #1914, .T. ) ;
#4471=FACE_OUTER_BOUND ( 'NONE', #5105, .T. ) ;
#4475=DIRECTION ( 'NONE',  ( 0.000000000000000000, -1.224646799147353700E-16, 1.000000000000000000 ) ) ;
#4476=CARTESIAN_POINT ( 'NONE',  ( 0.3528850351813199726, -0.3340780101605776986, -0.02497973507596915055 ) ) ;
#4479=CARTESIAN_POINT ( 'NONE',  ( 0.3321022367507226458, 0.2411754471855206694, -0.1728230530388957520 ) ) ;
#4487=CARTESIAN_POINT ( 'NONE',  ( 0.3483227611829848303, -0.1704774416898505729, -0.2952755905511810774 ) ) ;
#4489=CARTESIAN_POINT ( 'NONE',  ( 0.02637295201093697167, 0.1704774416898497680, -0.2952755905511810774 ) ) ;
#4491=CARTESIAN_POINT ( 'NONE',  ( 0.4685039370078740717, 0.000000000000000000, 0.000000000000000000 ) ) ;
#4508=CARTESIAN_POINT ( 'NONE',  ( 0.003035684155427131534, 0.2845908893795032757, 0.09762530132584859577 ) ) ;
#4510=CARTESIAN_POINT ( 'NONE',  ( 0.02637295201093707228, -0.1704774416898499345, 0.2952755905511811330 ) ) ;
#4518=CARTESIAN_POINT ( 'NONE',  ( 0.3565422270302655572, 0.1673297761639317704, -0.3007275071673040645 ) ) ;
#4519=CARTESIAN_POINT ( 'NONE',  ( 0.3442723180357430413, -0.1814473180894617399, 0.2762752072743029363 ) ) ;
#4522=AXIS2_PLACEMENT_3D ( 'NONE', #4415, #3563, #1671 ) ;
#4534=DIRECTION ( 'NONE',  ( 0.000000000000000000, 0.000000000000000000, -1.000000000000000000 ) ) ;
#4536=CARTESIAN_POINT ( 'NONE',  ( -5.972582710757682675E-17, -0.2484822268960368286, 0.1601673393405688428 ) ) ;
#4542=DIRECTION ( 'NONE',  ( -1.000000000000000000, -0.000000000000000000, -0.000000000000000000 ) ) ;
#4544=CARTESIAN_POINT ( 'NONE',  ( 0.000000000000000000, 0.000000000000000000, 0.000000000000000000 ) ) ;
#4546=DIRECTION ( 'NONE',  ( 0.000000000000000000, -0.8660254037844379305, 0.5000000000000013323 ) ) ;
#4547=ADVANCED_FACE ( 'NONE', ( #6380 ), #68, .F. ) ;
#4552=DIRECTION ( 'NONE',  ( 0.000000000000000000, 0.000000000000000000, 1.000000000000000000 ) ) ;
#4555=EDGE_LOOP ( 'NONE', ( #3151, #7013, #2014, #1779 ) ) ;
#4563=CARTESIAN_POINT ( 'NONE',  ( 0.3391892065151629332, -0.1136516277932338725, -0.2952755905511810774 ) ) ;
#4565=CARTESIAN_POINT ( 'NONE',  ( 0.01834252172841625839, 0.1843865549457985864, -0.2711842997036481573 ) ) ;
#4574=DIRECTION ( 'NONE',  ( 0.000000000000000000, 0.000000000000000000, 1.000000000000000000 ) ) ;
#4576=AXIS2_PLACEMENT_3D ( 'NONE', #3363, #4586, #7406 ) ;
#4577=CARTESIAN_POINT ( 'NONE',  ( 0.003035684155427232581, -0.2268414356900468332, 0.1976502892253331478 ) ) ;
#4586=DIRECTION ( 'NONE',  ( 1.000000000000000000, 0.000000000000000000, 0.000000000000000000 ) ) ;
#4588=EDGE_CURVE ( 'NONE', #4449, #1388, #6284, .T. ) ;
#4592=VERTEX_POINT ( 'NONE', #4159 ) ;
#4600=CARTESIAN_POINT ( 'NONE',  ( 0.004822332172886080806, 0.2197023059474403073, -0.2100156246613533173 ) ) ;
#4608=DIRECTION ( 'NONE',  ( -0.000000000000000000, 0.000000000000000000, -1.000000000000000000 ) ) ;
#4617=CARTESIAN_POINT ( 'NONE',  ( 0.3585664987351884214, -0.1764010263750315499, -0.3019340449705225082 ) ) ;
#4623=CARTESIAN_POINT ( 'NONE',  ( 0.3496779274129794279, -0.3447056852546012129, -0.006496579416451788574 ) ) ;
#4628=ORIENTED_EDGE ( 'NONE', *, *, #1441, .T. ) ;
#4631=CARTESIAN_POINT ( 'NONE',  ( 0.3485373078438441796, 0.2031105961982143382, -0.2516016230262507203 ) ) ;
#4656=CARTESIAN_POINT ( 'NONE',  ( 0.3581828924050327045, -0.3486337532542230222, -1.123169198254405176E-18 ) ) ;
#4661=CIRCLE ( 'NONE', #885, 0.2362204724409449064 ) ;
#4662=EDGE_CURVE ( 'NONE', #4592, #4449, #1813, .T. ) ;
#4679=AXIS2_PLACEMENT_3D ( 'NONE', #1735, #2309, #1090 ) ;
#4681=ORIENTED_EDGE ( 'NONE', *, *, #900, .F. ) ;
#4683=CARTESIAN_POINT ( 'NONE',  ( 0.3585665126877357611, -0.3496831043983833487, 0.001800812819183493984 ) ) ;
#4688=( GEOMETRIC_REPRESENTATION_CONTEXT ( 3 ) GLOBAL_UNCERTAINTY_ASSIGNED_CONTEXT ( ( #464 ) ) GLOBAL_UNIT_ASSIGNED_CONTEXT ( ( #7315, #2018, #2055 ) ) REPRESENTATION_CONTEXT ( 'NONE', 'WORKASPACE' ) );
#4691=CARTESIAN_POINT ( 'NONE',  ( 0.3391892065151629332, 0.3125419764313920323, 0.04921259842519686012 ) ) ;
#4692=CARTESIAN_POINT ( 'NONE',  ( 0.3528999085283635040, 0.1454870853231265693, 0.3018102362147644380 ) ) ;
#4696=VERTEX_POINT ( 'NONE', #2026 ) ;
#4703=VERTEX_POINT ( 'NONE', #192 ) ;
#4706=CARTESIAN_POINT ( 'NONE',  ( 0.3531509790457915132, 0.1471070558423459573, 0.3018164037399326816 ) ) ;
#4717=ORIENTED_EDGE ( 'NONE', *, *, #7147, .T. ) ;
#4719=CARTESIAN_POINT ( 'NONE',  ( 0.3442723180356911383, -0.3299850069800938646, -0.01900038327687023423 ) ) ;
#4725=CARTESIAN_POINT ( 'NONE',  ( 0.3483227611829846637, 0.1704774416898499345, 0.2952755905511810774 ) ) ;
#4726=( BOUNDED_SURFACE ( )  B_SPLINE_SURFACE ( 3, 2, ( 
 ( #1475, #5558, #6162 ),
 ( #917, #846, #5483 ),
 ( #317, #3245, #239 ),
 ( #2634, #4975, #5595 ),
 ( #2671, #1371, #5443 ),
 ( #3717, #202, #2524 ),
 ( #4854, #1951, #6058 ),
 ( #1060, #3398, #4617 ) ),
 .UNSPECIFIED., .F., .F., .F. ) 
 B_SPLINE_SURFACE_WITH_KNOTS ( ( 4, 2, 2, 4 ),
 ( 3, 3 ),
 ( 0.03552366018096265315, 0.03995354946645690575, 0.04216849410920403551, 0.04438343875195116528 ),
 ( 0.000000000000000000, 1.000000000000000000 ),
 .UNSPECIFIED. ) 
 GEOMETRIC_REPRESENTATION_ITEM ( )  RATIONAL_B_SPLINE_SURFACE ( (
 ( 1.000000000000000000, 0.8047780977832075244, 1.000000000000000000),
 ( 1.000000000000000000, 0.8123789484488428414, 1.000000000000000000),
 ( 1.000000000000000000, 0.8190677874188468932, 1.000000000000000000),
 ( 1.000000000000000000, 0.8191929099079664489, 1.000000000000000000),
 ( 1.000000000000000000, 0.8176081235728045460, 1.000000000000000000),
 ( 1.000000000000000000, 0.8122952617572927192, 1.000000000000000000),
 ( 1.000000000000000000, 0.8086306736854887989, 1.000000000000000000),
 ( 1.000000000000000000, 0.8047712637616463160, 1.000000000000000000) ) ) 
 REPRESENTATION_ITEM ( '' )  SURFACE ( )  );
#4728=CARTESIAN_POINT ( 'NONE',  ( 0.3306743754077733355, 0.2557161625347751932, 0.1476377952755905942 ) ) ;
#4733=CARTESIAN_POINT ( 'NONE',  ( 0.3483227611829848303, -0.1704774416898505729, -0.2952755905511810774 ) ) ;
#4742=EDGE_LOOP ( 'NONE', ( #674, #6253, #5214, #2038 ) ) ;
#4749=CARTESIAN_POINT ( 'NONE',  ( 0.3585665266928871331, 0.1764011776056260972, 0.3019340455778471433 ) ) ;
#4759=VERTEX_POINT ( 'NONE', #3204 ) ;
#4760=CARTESIAN_POINT ( 'NONE',  ( 0.3585569128062319755, -0.1733077889112134284, -0.3036897776982950825 ) ) ;
#4776=ADVANCED_FACE ( 'NONE', ( #504 ), #3975, .F. ) ;
#4781=EDGE_LOOP ( 'NONE', ( #3746, #1098, #1403, #3515 ) ) ;
#4811=ADVANCED_FACE ( 'NONE', ( #4471 ), #5226, .T. ) ;
#4815=DIRECTION ( 'NONE',  ( 0.000000000000000000, 0.5000000000000008882, -0.8660254037844380415 ) ) ;
#4820=CARTESIAN_POINT ( 'NONE',  ( 0.3425764178929368020, -0.2322094954269898481, 0.2008802154383053373 ) ) ;
#4821=VERTEX_POINT ( 'NONE', #3857 ) ;
#4836=( NAMED_UNIT ( * ) PLANE_ANGLE_UNIT ( ) SI_UNIT ( $, .RADIAN. ) );
#4851=ADVANCED_FACE ( 'NONE', ( #2665 ), #7362, .T. ) ;
#4854=CARTESIAN_POINT ( 'NONE',  ( 0.3442725010713152956, -0.1485386763991280168, -0.2952755905511810774 ) ) ;
#4857=CARTESIAN_POINT ( 'NONE',  ( 0.02637295201093723881, -0.1704774416898505729, -0.2952755905511810774 ) ) ;
#4872=CARTESIAN_POINT ( 'NONE',  ( 0.3403864257300880936, 0.2851194846584802489, 0.09670974744601845696 ) ) ;
#4881=CARTESIAN_POINT ( 'NONE',  ( 0.02637295201093707228, -0.1704774416898499345, 0.2952755905511811330 ) ) ;
#4885=CARTESIAN_POINT ( 'NONE',  ( 0.3391892065151629332, -0.1136516277932332758, 0.2952755905511811885 ) ) ;
#4893=CARTESIAN_POINT ( 'NONE',  ( 0.3505602286436571569, 0.3409548833797004797, 4.673058124370679309E-18 ) ) ;
#4894=CARTESIAN_POINT ( 'NONE',  ( 0.002513486811083437498, 0.2845799557467908469, -0.09764423893321776127 ) ) ;
#4904=EDGE_CURVE ( 'NONE', #7446, #6349, #5764, .T. ) ;
#4919=( CONVERSION_BASED_UNIT ( 'INCH', #3074 ) LENGTH_UNIT ( ) NAMED_UNIT ( #3354 ) );
#4926=CARTESIAN_POINT ( 'NONE',  ( 0.3997746709170348356, 0.000000000000000000, 0.000000000000000000 ) ) ;
#4934=CIRCLE ( 'NONE', #6395, 0.1982677165354330695 ) ;
#4938=B_SPLINE_CURVE_WITH_KNOTS ( 'NONE', 3,
 ( #6237, #6951, #468, #4010, #992, #5638 ),
 .UNSPECIFIED., .F., .F.,
 ( 4, 2, 4 ),
 ( 0.004466737480205772853, 0.006712681563759903200, 0.008958625647314033547 ),
 .UNSPECIFIED. ) ;
#4940=CYLINDRICAL_SURFACE ( 'NONE', #7294, 0.2362204724409449064 ) ;
#4946=ORIENTED_EDGE ( 'NONE', *, *, #484, .T. ) ;
#4953=ORIENTED_EDGE ( 'NONE', *, *, #4112, .T. ) ;
#4968=ORIENTED_EDGE ( 'NONE', *, *, #4105, .F. ) ;
#4971=CARTESIAN_POINT ( 'NONE',  ( 0.3574299024618897702, 0.3465649303883613364, 6.884133197150707104E-16 ) ) ;
#4975=CARTESIAN_POINT ( 'NONE',  ( 0.3387180295041032907, -0.02886098700874997411, -0.2952755905511810219 ) ) ;
#4977=EDGE_LOOP ( 'NONE', ( #4407, #3379, #5983, #4681, #7272 ) ) ;
#4980=CIRCLE ( 'NONE', #1305, 0.03543307086614165546 ) ;
#4994=AXIS2_PLACEMENT_3D ( 'NONE', #5910, #3528, #1178 ) ;
#5001=CARTESIAN_POINT ( 'NONE',  ( 0.3483227611829846637, -0.1704774416898499345, 0.2952755905511811330 ) ) ;
#5009=CARTESIAN_POINT ( 'NONE',  ( 0.4685039370078740717, 0.1704774416898497680, -0.2952755905511810774 ) ) ;
#5014=B_SPLINE_CURVE_WITH_KNOTS ( 'NONE', 3,
 ( #1042, #5645, #1102, #3414, #445, #5754, #4563, #401, #4487 ),
 .UNSPECIFIED., .F., .F.,
 ( 4, 2, 1, 2, 4 ),
 ( 0.000000000000000000, 0.002165063509461097064, 0.004330127018922194128, 0.006495190528383291625, 0.008660254037844388256 ),
 .UNSPECIFIED. ) ;
#5024=EDGE_LOOP ( 'NONE', ( #2233, #7066 ) ) ;
#5026=CARTESIAN_POINT ( 'NONE',  ( 0.3585569128062318645, 0.1733077889112127901, 0.3036897776982951380 ) ) ;
#5035=AXIS2_PLACEMENT_3D ( 'NONE', #5131, #3945, #4552 ) ;
#5053=CARTESIAN_POINT ( 'NONE',  ( 0.4330708661417324024, 5.520553484345353405E-17, -0.4507874015748032370 ) ) ;
#5093=CARTESIAN_POINT ( 'NONE',  ( 0.3403864257301138507, 0.2263128404110440195, -0.1985658431051529893 ) ) ;
#5095=CARTESIAN_POINT ( 'NONE',  ( 0.3337354549120238878, -0.2261274626982048841, 0.1988869267224354920 ) ) ;
#5104=DIRECTION ( 'NONE',  ( 0.000000000000000000, 0.000000000000000000, -1.000000000000000000 ) ) ;
#5105=EDGE_LOOP ( 'NONE', ( #1746, #4095, #1479 ) ) ;
#5110=VERTEX_POINT ( 'NONE', #7349 ) ;
#5117=CARTESIAN_POINT ( 'NONE',  ( 0.000000000000000000, 2.892866454678787531E-17, -0.2362204724409449064 ) ) ;
#5131=CARTESIAN_POINT ( 'NONE',  ( 0.4685039370078740717, 0.000000000000000000, 0.000000000000000000 ) ) ;
#5135=CARTESIAN_POINT ( 'NONE',  ( 0.3387177083556421331, 0.2412911239081777792, -0.1726226950780199998 ) ) ;
#5136=VECTOR ( 'NONE', #1238, 39.37007874015748143 ) ;
#5143=DIRECTION ( 'NONE',  ( -1.000000000000000000, -0.000000000000000000, -0.000000000000000000 ) ) ;
#5156=CARTESIAN_POINT ( 'NONE',  ( 0.3483227611829846082, 0.1704774416898497680, -0.2952755905511810774 ) ) ;
#5165=CARTESIAN_POINT ( 'NONE',  ( 0.3410249605999410294, 1.062103031354818709E-12, 0.3014927230551906479 ) ) ;
#5166=AXIS2_PLACEMENT_3D ( 'NONE', #418, #2134, #2741 ) ;
#5169=CARTESIAN_POINT ( 'NONE',  ( 0.000000000000000000, 0.000000000000000000, 0.000000000000000000 ) ) ;
#5171=CARTESIAN_POINT ( 'NONE',  ( 0.02637295201093697167, 0.1704774416898497680, -0.2952755905511810774 ) ) ;
#5176=CARTESIAN_POINT ( 'NONE',  ( 0.3322361761492156895, 0.2866471735582875047, -0.09406371265339424914 ) ) ;
#5184=CARTESIAN_POINT ( 'NONE',  ( 0.3483227611829846637, -0.1704774416898499345, 0.2952755905511811330 ) ) ;
#5192=DIRECTION ( 'NONE',  ( 1.000000000000000000, 0.000000000000000000, -0.000000000000000000 ) ) ;
#5205=CARTESIAN_POINT ( 'NONE',  ( 0.3398312250857989381, -0.1962691648279019652, 0.2506030156613254789 ) ) ;
#5214=ORIENTED_EDGE ( 'NONE', *, *, #5280, .F. ) ;
#5226=CONICAL_SURFACE ( 'NONE', #6210, 0.2952755905511810774, 1.047197551196600518 ) ;
#5246=CARTESIAN_POINT ( 'NONE',  ( 0.3425764178929367465, 0.2322094954269895706, -0.2008802154383052541 ) ) ;
#5264=CARTESIAN_POINT ( 'NONE',  ( 0.3561392902752972267, 0.1723302545757742221, 0.2984847566065203517 ) ) ;
#5280=EDGE_CURVE ( 'NONE', #4821, #3761, #4661, .T. ) ;
#5294=CARTESIAN_POINT ( 'NONE',  ( 0.3391892065151627111, 0.1988903486381581598, -0.2460629921259842312 ) ) ;
#5309=CARTESIAN_POINT ( 'NONE',  ( 0.3306743754077736130, -0.2557161625347754708, 0.1476377952755905387 ) ) ;
#5310=EDGE_LOOP ( 'NONE', ( #4265, #543, #1712 ) ) ;
#5326=ADVANCED_FACE ( 'NONE', ( #1212 ), #5776, .T. ) ;
#5335=CARTESIAN_POINT ( 'NONE',  ( 0.01171324505787584534, -0.3130206113228972131, -0.04838357847483532731 ) ) ;
#5340=UNCERTAINTY_MEASURE_WITH_UNIT (LENGTH_MEASURE( 1.000000000000000082E-05 ), #4919, 'distance_accuracy_value', 'NONE');
#5344=AXIS2_PLACEMENT_3D ( 'NONE', #6190, #4431, #2098 ) ;
#5361=ORIENTED_EDGE ( 'NONE', *, *, #5949, .F. ) ;
#5364=AXIS2_PLACEMENT_3D ( 'NONE', #126, #7078, #1790 ) ;
#5372=VECTOR ( 'NONE', #4069, 39.37007874015748143 ) ;
#5375=B_SPLINE_CURVE_WITH_KNOTS ( 'NONE', 3,
 ( #482, #2153, #6929, #1570, #2798, #2867 ),
 .UNSPECIFIED., .F., .F.,
 ( 4, 2, 4 ),
 ( 2.380732026380333730E-07, 0.002190927868076681349, 0.004381617662950723809 ),
 .UNSPECIFIED. ) ;
#5378=CARTESIAN_POINT ( 'NONE',  ( 0.3465694189147311421, -0.3147628225698668736, -0.04536598007755129891 ) ) ;
#5398=CARTESIAN_POINT ( 'NONE',  ( 0.3528850351813196395, -0.1886720902358828833, 0.2768301761068310274 ) ) ;
#5411=EDGE_LOOP ( 'NONE', ( #1165, #4367, #3111, #3300, #5755 ) ) ;
#5424=CARTESIAN_POINT ( 'NONE',  ( 0.3565325103478086954, -0.1673557731150450700, -0.3006824791271353603 ) ) ;
#5437=CARTESIAN_POINT ( 'NONE',  ( 0.002513486811083454845, 0.2268523693227592619, 0.1976313516179636909 ) ) ;
#5438=ORIENTED_EDGE ( 'NONE', *, *, #1974, .F. ) ;
#5443=CARTESIAN_POINT ( 'NONE',  ( 0.3426148638729746843, -0.05855635169929876427, -0.3015406112749626777 ) ) ;
#5447=ORIENTED_EDGE ( 'NONE', *, *, #4588, .F. ) ;
#5453=CARTESIAN_POINT ( 'NONE',  ( 0.3581828924050327045, -0.3486337532542230222, -1.123169198254405176E-18 ) ) ;
#5454=CARTESIAN_POINT ( 'NONE',  ( 0.3388536909603142577, 0.2250264928541962084, 0.2007938624298919450 ) ) ;
#5459=SHAPE_REPRESENTATION_RELATIONSHIP ( 'NONE' , 'NONE' ,  #7075, #314 ) ;
#5461=CARTESIAN_POINT ( 'NONE',  ( 0.3496875272944831026, -0.3447318307381757041, 0.006541864722391225496 ) ) ;
#5465=B_SPLINE_CURVE_WITH_KNOTS ( 'NONE', 3,
 ( #5481, #275, #916, #4894, #6057, #6119 ),
 .UNSPECIFIED., .F., .F.,
 ( 4, 2, 4 ),
 ( 2.380732026382070147E-07, 0.002190927868076674410, 0.004381617662950710798 ),
 .UNSPECIFIED. ) ;
#5481=CARTESIAN_POINT ( 'NONE',  ( 0.02637295201093722841, 0.3409548833797004797, 3.882420715168025960E-18 ) ) ;
#5483=CARTESIAN_POINT ( 'NONE',  ( 0.3479975484506714345, 0.1192183696110101915, -0.3017044215715822819 ) ) ;
#5498=VERTEX_POINT ( 'NONE', #3792 ) ;
#5518=FACE_OUTER_BOUND ( 'NONE', #1677, .T. ) ;
#5530=DIRECTION ( 'NONE',  ( 0.000000000000000000, 1.000000000000000000, -1.001543065824774208E-16 ) ) ;
#5535=EDGE_CURVE ( 'NONE', #4759, #4696, #6846, .T. ) ;
#5536=CARTESIAN_POINT ( 'NONE',  ( 0.3337354549120238878, 0.2853048623713461129, 0.09638866382874489158 ) ) ;
#5554=CARTESIAN_POINT ( 'NONE',  ( 0.4330708661417324024, 0.000000000000000000, 0.000000000000000000 ) ) ;
#5558=CARTESIAN_POINT ( 'NONE',  ( 0.3565325281581928074, 0.1767208741530144900, -0.2952755905511811330 ) ) ;
#5561=ORIENTED_EDGE ( 'NONE', *, *, #7472, .F. ) ;
#5562=CARTESIAN_POINT ( 'NONE',  ( 0.3483227611829846637, -0.1704774416898499345, 0.2952755905511811330 ) ) ;
#5568=CARTESIAN_POINT ( 'NONE',  ( 0.3574269917172687161, -0.3465569331832414335, -9.402262055513304185E-15 ) ) ;
#5580=EDGE_CURVE ( 'NONE', #5905, #1170, #3290, .T. ) ;
#5584=CARTESIAN_POINT ( 'NONE',  ( 0.000000000000000000, -0.2557161625347748601, 0.1476377952755911216 ) ) ;
#5585=ADVANCED_FACE ( 'NONE', ( #6279 ), #3215, .F. ) ;
#5592=DIRECTION ( 'NONE',  ( 0.000000000000000000, 0.000000000000000000, -1.000000000000000000 ) ) ;
#5595=CARTESIAN_POINT ( 'NONE',  ( 0.3409815385080205985, -0.02878389060673587282, -0.3014914578570770387 ) ) ;
#5603=PLANE ( 'NONE',  #6623 ) ;
#5622=EDGE_CURVE ( 'NONE', #4413, #2064, #1618, .T. ) ;
#5633=CARTESIAN_POINT ( 'NONE',  ( 0.3483227611829846637, 0.1704774416898499345, 0.2952755905511810774 ) ) ;
#5638=CARTESIAN_POINT ( 'NONE',  ( 0.3581828924050323715, -0.1743168766271109560, 0.3019256869348722616 ) ) ;
#5642=ORIENTED_EDGE ( 'NONE', *, *, #1974, .T. ) ;
#5645=CARTESIAN_POINT ( 'NONE',  ( 0.3432736861146659657, 0.1420645347415414039, -0.2952755905511810219 ) ) ;
#5669=CARTESIAN_POINT ( 'NONE',  ( 8.136851934253910637E-18, -0.02882762270234999827, 0.2952755905511811330 ) ) ;
#5676=EDGE_CURVE ( 'NONE', #4304, #733, #2015, .T. ) ;
#5679=CARTESIAN_POINT ( 'NONE',  ( 0.3322361761492158561, -0.2866471735583170366, 0.09406371265334383114 ) ) ;
#5681=ORIENTED_EDGE ( 'NONE', *, *, #3887, .T. ) ;
#5682=ORIENTED_EDGE ( 'NONE', *, *, #7340, .F. ) ;
#5690=CARTESIAN_POINT ( 'NONE',  ( 0.3432736861146661878, -0.3267484299055466446, 0.02460629921259842312 ) ) ;
#5696=ORIENTED_EDGE ( 'NONE', *, *, #1919, .F. ) ;
#5710=CARTESIAN_POINT ( 'NONE',  ( 0.3483227611829849413, -0.3409548833797009237, 0.000000000000000000 ) ) ;
#5731=CARTESIAN_POINT ( 'NONE',  ( 0.4685039370078740717, 0.000000000000000000, 0.000000000000000000 ) ) ;
#5733=CARTESIAN_POINT ( 'NONE',  ( 0.01171324505787554697, -0.1984117137466534231, 0.2468920120763462012 ) ) ;
#5741=FACE_OUTER_BOUND ( 'NONE', #2297, .T. ) ;
#5754=CARTESIAN_POINT ( 'NONE',  ( 0.3336175750056032951, -0.05682581389661717219, -0.2952755905511811330 ) ) ;
#5755=ORIENTED_EDGE ( 'NONE', *, *, #2013, .F. ) ;
#5756=CARTESIAN_POINT ( 'NONE',  ( 0.3585665126877356501, 0.3496831043983829046, -0.001800812819183686539 ) ) ;
#5759=DIMENSIONAL_EXPONENTS ( 1.000000000000000000, 0.000000000000000000, 0.000000000000000000, 0.000000000000000000, 0.000000000000000000, 0.000000000000000000, 0.000000000000000000 ) ;
#5764=B_SPLINE_CURVE_WITH_KNOTS ( 'NONE', 3,
 ( #2174, #6156, #7323, #4508, #6841, #912, #1593, #1022 ),
 .UNSPECIFIED., .F., .F.,
 ( 4, 2, 2, 4 ),
 ( 0.004381617662950689981, 0.005472867551409524994, 0.006564117439868360007, 0.008746617216786028298 ),
 .UNSPECIFIED. ) ;
#5769=( BOUNDED_SURFACE ( )  B_SPLINE_SURFACE ( 3, 2, ( 
 ( #2684, #3107, #5026 ),
 ( #2571, #3729, #6634 ),
 ( #6136, #5454, #2123 ),
 ( #1965, #216, #857 ),
 ( #5536, #4872, #4457 ),
 ( #7234, #1528, #4294 ),
 ( #2007, #6026, #779 ),
 ( #4338, #7194, #5756 ) ),
 .UNSPECIFIED., .F., .F., .F. ) 
 B_SPLINE_SURFACE_WITH_KNOTS ( ( 4, 2, 2, 4 ),
 ( 3, 3 ),
 ( 0.03551798592901333346, 0.03994769179990642627, 0.04216254473535296921, 0.04437739767079951908 ),
 ( 0.000000000000000000, 1.000000000000000000 ),
 .UNSPECIFIED. ) 
 GEOMETRIC_REPRESENTATION_ITEM ( )  RATIONAL_B_SPLINE_SURFACE ( (
 ( 1.000000000000000000, 0.8047781103519391355, 1.000000000000000000),
 ( 1.000000000000000000, 0.8123785826169017676, 1.000000000000000000),
 ( 1.000000000000000000, 0.8190671539036440407, 1.000000000000000000),
 ( 1.000000000000000000, 0.8191932076449144340, 1.000000000000000000),
 ( 1.000000000000000000, 0.8176085094066379844, 1.000000000000000000),
 ( 1.000000000000000000, 0.8122955484014008354, 1.000000000000000000),
 ( 1.000000000000000000, 0.8086308001280846369, 1.000000000000000000),
 ( 1.000000000000000000, 0.8047712537969720081, 1.000000000000000000) ) ) 
 REPRESENTATION_ITEM ( '' )  SURFACE ( )  );
#5771=DIRECTION ( 'NONE',  ( -1.000000000000000000, -0.000000000000000000, -0.000000000000000000 ) ) ;
#5775=PLANE ( 'NONE',  #1243 ) ;
#5776=CONICAL_SURFACE ( 'NONE', #4302, 0.2952755905511810774, 1.047197551196600518 ) ;
#5783=CARTESIAN_POINT ( 'NONE',  ( 0.3398312250857988270, 0.1962691648278992451, -0.2506030156613296422 ) ) ;
#5784=CARTESIAN_POINT ( 'NONE',  ( 0.3391216574608478806, -0.3159523085418498023, 0.04330572993920116937 ) ) ;
#5789=VERTEX_POINT ( 'NONE', #312 ) ;
#5794=AXIS2_PLACEMENT_3D ( 'NONE', #4926, #2025, #6719 ) ;
#5795=STYLED_ITEM('',(#7587),#1545);
#5817=ORIENTED_EDGE ( 'NONE', *, *, #3403, .T. ) ;
#5825=CARTESIAN_POINT ( 'NONE',  ( 0.3483227611829848303, 0.3409548833797004797, 0.000000000000000000 ) ) ;
#5832=CARTESIAN_POINT ( 'NONE',  ( 0.3483227611829846082, 0.1704774416898497680, -0.2952755905511810774 ) ) ;
#5835=ADVANCED_FACE ( 'NONE', ( #6657 ), #1373, .T. ) ;
#5838=AXIS2_PLACEMENT_3D ( 'NONE', #3790, #6662, #3755 ) ;
#5845=ADVANCED_FACE ( 'NONE', ( #2668 ), #2347, .T. ) ;
#5849=CARTESIAN_POINT ( 'NONE',  ( 0.3410249605999410294, -1.062517223525361548E-12, -0.3014927230551905368 ) ) ;
#5853=VERTEX_POINT ( 'NONE', #764 ) ;
#5864=CARTESIAN_POINT ( 'NONE',  ( 0.3510870379221574522, 0.1475852640829200257, 0.2952755905511810774 ) ) ;
#5886=CARTESIAN_POINT ( 'NONE',  ( 0.3432736861146661322, -0.1846838951640041859, 0.2706692913385828625 ) ) ;
#5892=ADVANCED_FACE ( 'NONE', ( #5741 ), #7231, .T. ) ;
#5895=EDGE_LOOP ( 'NONE', ( #6433, #6764, #4953, #5696, #1799 ) ) ;
#5905=VERTEX_POINT ( 'NONE', #5633 ) ;
#5910=CARTESIAN_POINT ( 'NONE',  ( 0.000000000000000000, 0.000000000000000000, 0.000000000000000000 ) ) ;
#5934=CARTESIAN_POINT ( 'NONE',  ( 0.3997746709170348356, 0.000000000000000000, 0.000000000000000000 ) ) ;
#5939=CARTESIAN_POINT ( 'NONE',  ( 0.4330708661417324024, 0.000000000000000000, 0.4507874015748032370 ) ) ;
#5944=B_SPLINE_CURVE_WITH_KNOTS ( 'NONE', 3,
 ( #1245, #5398, #1285, #4820, #2321, #3051, #163, #1913, #74, #4656 ),
 .UNSPECIFIED., .F., .F.,
 ( 4, 2, 2, 2, 4 ),
 ( 0.000000000000000000, 0.002239656411828512290, 0.004479312823657024580, 0.006718969235485537303, 0.008958625647314049159 ),
 .UNSPECIFIED. ) ;
#5947=CARTESIAN_POINT ( 'NONE',  ( 0.3581828924050323715, 0.1743168766271107895, -0.3019256869348722061 ) ) ;
#5949=EDGE_CURVE ( 'NONE', #6192, #3692, #6490, .T. ) ;
#5958=CARTESIAN_POINT ( 'NONE',  ( 0.3403864257300625029, -0.2851194846584945153, -0.09670974744601064377 ) ) ;
#5964=CARTESIAN_POINT ( 'NONE',  ( 0.3336175750056032396, 0.2841290694830835850, 0.09842519685039366473 ) ) ;
#5967=CONICAL_SURFACE ( 'NONE', #5838, 0.1982677165354330695, 0.7853981633974415066 ) ;
#5981=ORIENTED_EDGE ( 'NONE', *, *, #6368, .F. ) ;
#5983=ORIENTED_EDGE ( 'NONE', *, *, #1483, .T. ) ;
#5986=CARTESIAN_POINT ( 'NONE',  ( 0.3391221370943153790, -0.1204748818123362597, 0.2952755905511811330 ) ) ;
#5993=ADVANCED_FACE ( 'NONE', ( #7364 ), #3360, .F. ) ;
#5997=CARTESIAN_POINT ( 'NONE',  ( 0.3479980290963871625, -0.2016732288369692816, -0.2541005850305417257 ) ) ;
#6006=CARTESIAN_POINT ( 'NONE',  ( 0.002549129251883240199, 0.05807386165065146072, -0.2952755905511810219 ) ) ;
#6016=CARTESIAN_POINT ( 'NONE',  ( 0.4330708661417324024, 0.000000000000000000, 0.000000000000000000 ) ) ;
#6026=CARTESIAN_POINT ( 'NONE',  ( 0.3510872220067180471, 0.3295092824291462330, 0.01982436236955231745 ) ) ;
#6034=CARTESIAN_POINT ( 'NONE',  ( 0.003035684155427393477, -0.2845908893795038308, -0.09762530132584867903 ) ) ;
#6037=ADVANCED_FACE ( 'NONE', ( #3435 ), #5775, .F. ) ;
#6057=CARTESIAN_POINT ( 'NONE',  ( -2.349015779708382802E-16, 0.2702383257424525453, -0.1224846707640857985 ) ) ;
#6058=CARTESIAN_POINT ( 'NONE',  ( 0.3531513458567848707, -0.1471090214728858203, -0.3018164116569697075 ) ) ;
#6069=ORIENTED_EDGE ( 'NONE', *, *, #3703, .F. ) ;
#6080=CARTESIAN_POINT ( 'NONE',  ( 0.01841426102874111140, 0.1429077274040426171, -0.2952755905511810219 ) ) ;
#6087=VERTEX_POINT ( 'NONE', #7056 ) ;
#6095=CARTESIAN_POINT ( 'NONE',  ( 0.3561392902752972267, -0.1723302545757742776, 0.2984847566065203517 ) ) ;
#6102=FACE_OUTER_BOUND ( 'NONE', #2235, .T. ) ;
#6114=CARTESIAN_POINT ( 'NONE',  ( 0.3410076799406683290, 0.2754140928391118348, 0.1259532371559686781 ) ) ;
#6118=CARTESIAN_POINT ( 'NONE',  ( 0.3527008206095850751, 0.3418447298186451655, 4.692841048826145323E-17 ) ) ;
#6119=CARTESIAN_POINT ( 'NONE',  ( 0.000000000000000000, 0.2557161625347749712, -0.1476377952755909551 ) ) ;
#6136=CARTESIAN_POINT ( 'NONE',  ( 0.3322361761492683696, 0.2247851515112334331, 0.2012118778978378431 ) ) ;
#6152=CARTESIAN_POINT ( 'NONE',  ( 0.02637295201093707228, -0.1704774416898499345, 0.2952755905511811330 ) ) ;
#6156=CARTESIAN_POINT ( 'NONE',  ( -1.704737175733852238E-16, 0.2629500981735131693, 0.1351082512106132616 ) ) ;
#6158=ORIENTED_EDGE ( 'NONE', *, *, #3456, .F. ) ;
#6162=CARTESIAN_POINT ( 'NONE',  ( 0.3585569304025113535, 0.1763492631043844516, -0.3019338371022697864 ) ) ;
#6165=ORIENTED_EDGE ( 'NONE', *, *, #5622, .T. ) ;
#6169=DIRECTION ( 'NONE',  ( 0.000000000000000000, -1.001543065824774208E-16, -1.000000000000000000 ) ) ;
#6190=CARTESIAN_POINT ( 'NONE',  ( 0.4685039370078740717, -0.1704774416898505729, -0.2952755905511810774 ) ) ;
#6192=VERTEX_POINT ( 'NONE', #4881 ) ;
#6198=CARTESIAN_POINT ( 'NONE',  ( 0.3336175750056034617, -0.2841290694830840846, -0.09842519685039370636 ) ) ;
#6206=LINE ( 'NONE', #968, #2170 ) ;
#6209=VERTEX_POINT ( 'NONE', #1314 ) ;
#6210=AXIS2_PLACEMENT_3D ( 'NONE', #3357, #2212, #3241 ) ;
#6214=ORIENTED_EDGE ( 'NONE', *, *, #1920, .T. ) ;
#6229=DIRECTION ( 'NONE',  ( -1.000000000000000000, -0.000000000000000000, -0.000000000000000000 ) ) ;
#6237=CARTESIAN_POINT ( 'NONE',  ( 0.3410249605999410294, 1.062103031354818709E-12, 0.3014927230551906479 ) ) ;
#6239=ORIENTED_EDGE ( 'NONE', *, *, #4026, .F. ) ;
#6240=CARTESIAN_POINT ( 'NONE',  ( 0.3388536909602617997, -0.2864058322153867353, 0.09448172812127884901 ) ) ;
#6252=ORIENTED_EDGE ( 'NONE', *, *, #134, .F. ) ;
#6253=ORIENTED_EDGE ( 'NONE', *, *, #1588, .T. ) ;
#6254=CARTESIAN_POINT ( 'NONE',  ( 0.3528999085283636150, -0.1454870853231272354, -0.3018102362147644380 ) ) ;
#6278=CARTESIAN_POINT ( 'NONE',  ( 0.3479980290964227452, 0.3208941761715193852, -0.04760384692076755769 ) ) ;
#6279=FACE_OUTER_BOUND ( 'NONE', #6847, .T. ) ;
#6284=B_SPLINE_CURVE_WITH_KNOTS ( 'NONE', 3,
 ( #7064, #4692, #1822, #1239, #3588, #1160 ),
 .UNSPECIFIED., .F., .F.,
 ( 4, 2, 4 ),
 ( 0.000000000000000000, 0.002233368740102886427, 0.004466737480205772853 ),
 .UNSPECIFIED. ) ;
#6286=ORIENTED_EDGE ( 'NONE', *, *, #5949, .T. ) ;
#6287=CARTESIAN_POINT ( 'NONE',  ( 0.3336175750056034617, -0.2841290694830839736, 0.09842519685039370636 ) ) ;
#6297=CARTESIAN_POINT ( 'NONE',  ( 0.004822332172886236931, -0.2197023059474404461, 0.2100156246613535393 ) ) ;
#6300=( BOUNDED_SURFACE ( )  B_SPLINE_SURFACE ( 3, 2, ( 
 ( #2426, #5424, #4760 ),
 ( #183, #1855, #5997 ),
 ( #3112, #4190, #6530 ),
 ( #1269, #6604, #2506 ),
 ( #3615, #5958, #2385 ),
 ( #7165, #5378, #712 ),
 ( #4719, #1311, #3659 ),
 ( #5461, #2348, #4683 ) ),
 .UNSPECIFIED., .F., .F., .F. ) 
 B_SPLINE_SURFACE_WITH_KNOTS ( ( 4, 2, 2, 4 ),
 ( 3, 3 ),
 ( 0.03551798592901340978, 0.03994769179990649566, 0.04216254473535303859, 0.04437739767079958153 ),
 ( 0.000000000000000000, 1.000000000000000000 ),
 .UNSPECIFIED. ) 
 GEOMETRIC_REPRESENTATION_ITEM ( )  RATIONAL_B_SPLINE_SURFACE ( (
 ( 1.000000000000000000, 0.8047781103519396906, 1.000000000000000000),
 ( 1.000000000000000000, 0.8123785826170297764, 1.000000000000000000),
 ( 1.000000000000000000, 0.8190671539034730664, 1.000000000000000000),
 ( 1.000000000000000000, 0.8191932076449999212, 1.000000000000000000),
 ( 1.000000000000000000, 0.8176085094066802839, 1.000000000000000000),
 ( 1.000000000000000000, 0.8122955484013585359, 1.000000000000000000),
 ( 1.000000000000000000, 0.8086308001281159452, 1.000000000000000000),
 ( 1.000000000000000000, 0.8047712537969721192, 1.000000000000000000) ) ) 
 REPRESENTATION_ITEM ( '' )  SURFACE ( )  );
#6302=DIRECTION ( 'NONE',  ( -1.000000000000000000, -0.000000000000000000, -0.000000000000000000 ) ) ;
#6310=CARTESIAN_POINT ( 'NONE',  ( 0.3410076799406688286, -0.2754140928391124454, -0.1259532371559686781 ) ) ;
#6345=ORIENTED_EDGE ( 'NONE', *, *, #2764, .F. ) ;
#6348=CARTESIAN_POINT ( 'NONE',  ( 0.3496875272944827695, -0.1667004943313752652, 0.3018174552735723437 ) ) ;
#6349=VERTEX_POINT ( 'NONE', #456 ) ;
#6368=EDGE_CURVE ( 'NONE', #725, #6192, #7404, .T. ) ;
#6378=CARTESIAN_POINT ( 'NONE',  ( 0.3410425348215777031, -0.2462961272004795532, -0.1763890642357578975 ) ) ;
#6380=FACE_OUTER_BOUND ( 'NONE', #2674, .T. ) ;
#6387=EDGE_LOOP ( 'NONE', ( #6549, #1224, #5438 ) ) ;
#6391=EDGE_LOOP ( 'NONE', ( #2894, #3055, #878, #1127, #5642, #6158 ) ) ;
#6395=AXIS2_PLACEMENT_3D ( 'NONE', #3390, #5771, #2779 ) ;
#6403=EDGE_CURVE ( 'NONE', #2762, #3843, #2750, .T. ) ;
#6406=DIRECTION ( 'NONE',  ( 1.000000000000000000, 0.000000000000000000, -0.000000000000000000 ) ) ;
#6422=CARTESIAN_POINT ( 'NONE',  ( 0.3410249605999410294, -1.062517223525361548E-12, -0.3014927230551905368 ) ) ;
#6433=ORIENTED_EDGE ( 'NONE', *, *, #3794, .F. ) ;
#6437=DIRECTION ( 'NONE',  ( 1.000000000000000000, 0.000000000000000000, -0.000000000000000000 ) ) ;
#6444=ADVANCED_FACE ( 'NONE', ( #7012, #1117 ), #1763, .T. ) ;
#6448=ADVANCED_FACE ( 'NONE', ( #93 ), #4052, .T. ) ;
#6451=CARTESIAN_POINT ( 'NONE',  ( 0.3483227611829846637, 0.1704774416898499345, 0.2952755905511810774 ) ) ;
#6490=B_SPLINE_CURVE_WITH_KNOTS ( 'NONE', 3,
 ( #4510, #3900, #6762, #3320, #5669, #4008 ),
 .UNSPECIFIED., .F., .F.,
 ( 4, 2, 4 ),
 ( 0.007897041933671775787, 0.01008815886328916570, 0.01227927579290655560 ),
 .UNSPECIFIED. ) ;
#6513=CARTESIAN_POINT ( 'NONE',  ( 0.3485777078273625817, 0.3195689143662219234, -0.04989192643193119531 ) ) ;
#6516=EDGE_LOOP ( 'NONE', ( #1287, #2801, #2200, #3187 ) ) ;
#6525=CARTESIAN_POINT ( 'NONE',  ( 0.000000000000000000, 0.2557161625347749712, -0.1476377952755909551 ) ) ;
#6526=ORIENTED_EDGE ( 'NONE', *, *, #4588, .T. ) ;
#6530=CARTESIAN_POINT ( 'NONE',  ( 0.3411151615605753085, -0.2304996462388200218, -0.2037536041052529223 ) ) ;
#6536=DIRECTION ( 'NONE',  ( -1.000000000000000000, 0.000000000000000000, -0.000000000000000000 ) ) ;
#6549=ORIENTED_EDGE ( 'NONE', *, *, #2492, .T. ) ;
#6552=EDGE_CURVE ( 'NONE', #5853, #5110, #262, .T. ) ;
#6577=CARTESIAN_POINT ( 'NONE',  ( 0.01168997831664858947, 0.1984671517595417711, 0.2467959906213527677 ) ) ;
#6604=CARTESIAN_POINT ( 'NONE',  ( 0.3387177083556159873, -0.2701412011614057196, -0.1226528954731239129 ) ) ;
#6612=CARTESIAN_POINT ( 'NONE',  ( 0.01178921041716498620, 0.1149842948508797008, -0.2952755905511810774 ) ) ;
#6615=CARTESIAN_POINT ( 'NONE',  ( 1.649606299212598381, 2.660472849486257786E-17, -0.1982677165354330695 ) ) ;
#6616=ORIENTED_EDGE ( 'NONE', *, *, #6784, .F. ) ;
#6623=AXIS2_PLACEMENT_3D ( 'NONE', #7266, #6169, #5530 ) ;
#6624=DIRECTION ( 'NONE',  ( -1.000000000000000000, -0.000000000000000000, -0.000000000000000000 ) ) ;
#6625=CARTESIAN_POINT ( 'NONE',  ( 0.002513486811083733702, -0.2268523693227597338, -0.1976313516179637741 ) ) ;
#6629=VERTEX_POINT ( 'NONE', #6525 ) ;
#6634=CARTESIAN_POINT ( 'NONE',  ( 0.3479980290963966549, 0.2016732288369792181, 0.2541005850305664282 ) ) ;
#6637=AXIS2_PLACEMENT_3D ( 'NONE', #7177, #3243, #5592 ) ;
#6657=FACE_OUTER_BOUND ( 'NONE', #311, .T. ) ;
#6662=DIRECTION ( 'NONE',  ( -1.000000000000000000, -0.000000000000000000, -0.000000000000000000 ) ) ;
#6667=ORIENTED_EDGE ( 'NONE', *, *, #2431, .T. ) ;
#6669=B_SPLINE_CURVE_WITH_KNOTS ( 'NONE', 3,
 ( #1002, #4452, #6702, #3293, #854, #1448 ),
 .UNSPECIFIED., .F., .F.,
 ( 4, 2, 4 ),
 ( 0.02625214965902978106, 0.02844383079405753134, 0.03063551192908527815 ),
 .UNSPECIFIED. ) ;
#6693=CARTESIAN_POINT ( 'NONE',  ( 0.000000000000000000, 0.000000000000000000, 0.000000000000000000 ) ) ;
#6702=CARTESIAN_POINT ( 'NONE',  ( 0.002479217192763490639, -0.05744896992510376693, -0.2952755905511810774 ) ) ;
#6718=CARTESIAN_POINT ( 'NONE',  ( 0.3336175750056032396, -0.05682581389661664484, 0.2952755905511811330 ) ) ;
#6719=DIRECTION ( 'NONE',  ( 0.000000000000000000, 0.000000000000000000, -1.000000000000000000 ) ) ;
#6731=CARTESIAN_POINT ( 'NONE',  ( 0.3527008206095850196, -0.1709223649093223885, 0.2960462201727743770 ) ) ;
#6737=FACE_OUTER_BOUND ( 'NONE', #6953, .T. ) ;
#6750=CARTESIAN_POINT ( 'NONE',  ( 0.3561390657006783811, -0.1723301304999994843, -0.2984845417009731050 ) ) ;
#6762=CARTESIAN_POINT ( 'NONE',  ( 0.01165389088405563781, -0.1143408654217081682, 0.2952755905511811885 ) ) ;
#6764=ORIENTED_EDGE ( 'NONE', *, *, #6403, .T. ) ;
#6784=EDGE_CURVE ( 'NONE', #4696, #6209, #5944, .T. ) ;
#6798=PRODUCT_DEFINITION_FORMATION_WITH_SPECIFIED_SOURCE ( 'ANY', '', #2452, .NOT_KNOWN. ) ;
#6799=CARTESIAN_POINT ( 'NONE',  ( 0.3561390657006783811, 0.1723301304999986516, -0.2984845417009731605 ) ) ;
#6806=CARTESIAN_POINT ( 'NONE',  ( 0.3391892065151630442, -0.3125419764313924764, -0.04921259842519686706 ) ) ;
#6812=ORIENTED_EDGE ( 'NONE', *, *, #3703, .T. ) ;
#6841=CARTESIAN_POINT ( 'NONE',  ( 0.004822332172886149328, 0.2917300191221098293, 0.08525996588982816260 ) ) ;
#6842=CIRCLE ( 'NONE', #7197, 0.2362204724409449064 ) ;
#6846=B_SPLINE_CURVE_WITH_KNOTS ( 'NONE', 3,
 ( #5562, #2564, #6731, #6095, #7335, #2639 ),
 .UNSPECIFIED., .F., .F.,
 ( 4, 2, 4 ),
 ( 0.000000000000000000, 0.0001677595217559109278, 0.0003355190435118218556 ),
 .UNSPECIFIED. ) ;
#6847=EDGE_LOOP ( 'NONE', ( #5, #1344, #6239, #6616 ) ) ;
#6848=CARTESIAN_POINT ( 'NONE',  ( 0.3565325103478086399, 0.3440765519545058160, 0.005406888575954027845 ) ) ;
#6863=CARTESIAN_POINT ( 'NONE',  ( 0.3410249605999788325, -0.02903799983316278366, -0.3014927230551917026 ) ) ;
#6867=LINE ( 'NONE', #5117, #1223 ) ;
#6872=B_SPLINE_CURVE_WITH_KNOTS ( 'NONE', 3,
 ( #7394, #4421, #6750, #1581, #2166, #1501 ),
 .UNSPECIFIED., .F., .F.,
 ( 4, 2, 4 ),
 ( -3.269571951031369869E-06, 0.0001651384380483837840, 0.0003335464480477989433 ),
 .UNSPECIFIED. ) ;
#6891=CARTESIAN_POINT ( 'NONE',  ( 0.3426144402834003788, -0.2318662757222078041, 0.2014770286013906619 ) ) ;
#6894=CONICAL_SURFACE ( 'NONE', #4576, 0.4629062255509093782, 1.221730476396037490 ) ;
#6897=ORIENTED_EDGE ( 'NONE', *, *, #1588, .F. ) ;
#6898=CARTESIAN_POINT ( 'NONE',  ( 0.000000000000000000, 0.000000000000000000, 0.000000000000000000 ) ) ;
#6900=DIRECTION ( 'NONE',  ( -1.000000000000000000, -0.000000000000000000, 0.000000000000000000 ) ) ;
#6904=CARTESIAN_POINT ( 'NONE',  ( 0.000000000000000000, 0.000000000000000000, 0.000000000000000000 ) ) ;
#6906=CARTESIAN_POINT ( 'NONE',  ( 0.01834252172841640063, -0.1843865549457986697, 0.2711842997036482683 ) ) ;
#6907=EDGE_CURVE ( 'NONE', #7025, #4703, #2923, .T. ) ;
#6910=DIRECTION ( 'NONE',  ( -0.000000000000000000, 0.000000000000000000, -1.000000000000000000 ) ) ;
#6921=CARTESIAN_POINT ( 'NONE',  ( 0.3426144402833972147, 0.2318662757222082205, -0.2014770286013785050 ) ) ;
#6922=CARTESIAN_POINT ( 'NONE',  ( 0.3479980290963757827, -0.3208941761713900997, 0.04760384692073289098 ) ) ;
#6925=VERTEX_POINT ( 'NONE', #803 ) ;
#6928=EDGE_CURVE ( 'NONE', #2762, #4592, #478, .T. ) ;
#6929=CARTESIAN_POINT ( 'NONE',  ( 0.01168997831664888090, -0.3129651733100090039, 0.04847959992982862204 ) ) ;
#6951=CARTESIAN_POINT ( 'NONE',  ( 0.3410249605999032263, -0.02920150297965336608, 0.3014927230551895931 ) ) ;
#6953=EDGE_LOOP ( 'NONE', ( #3014, #2459, #585, #1724, #5361 ) ) ;
#6955=CIRCLE ( 'NONE', #4522, 0.2952755905511810774 ) ;
#6962=CARTESIAN_POINT ( 'NONE',  ( 0.3528971332113847725, 0.3341112492250003507, -0.02492269209175868722 ) ) ;
#6973=CARTESIAN_POINT ( 'NONE',  ( 0.02637295201093703412, 0.1704774416898499345, 0.2952755905511810774 ) ) ;
#6975=DIRECTION ( 'NONE',  ( -1.000000000000000000, -0.000000000000000000, -0.000000000000000000 ) ) ;
#6976=CARTESIAN_POINT ( 'NONE',  ( 0.3432736861146661322, 0.3267484299055462005, -0.02460629921259842659 ) ) ;
#6987=CARTESIAN_POINT ( 'NONE',  ( 0.3432736861146659657, 0.1846838951640041582, 0.2706692913385826960 ) ) ;
#6995=EDGE_CURVE ( 'NONE', #7262, #5789, #2830, .T. ) ;
#6997=CARTESIAN_POINT ( 'NONE',  ( 0.3581828924050323715, 0.1743168766271107895, -0.3019256869348722061 ) ) ;
#7002=CIRCLE ( 'NONE', #3102, 0.03543307086614165546 ) ;
#7004=CARTESIAN_POINT ( 'NONE',  ( 0.3387173876318818611, 0.02883917696872971906, 0.2952755905511811330 ) ) ;
#7006=ADVANCED_FACE ( 'NONE', ( #676 ), #6300, .F. ) ;
#7012=FACE_BOUND ( 'NONE', #5024, .T. ) ;
#7013=ORIENTED_EDGE ( 'NONE', *, *, #3, .T. ) ;
#7023=DIRECTION ( 'NONE',  ( 0.000000000000000000, 0.8660254037844375974, -0.5000000000000018874 ) ) ;
#7025=VERTEX_POINT ( 'NONE', #4400 ) ;
#7032=CARTESIAN_POINT ( 'NONE',  ( 0.3410076799406683845, 0.2467857494855107137, -0.1755389823809322958 ) ) ;
#7039=CARTESIAN_POINT ( 'NONE',  ( 0.3496875412996344190, 0.1780314126850971457, 0.2952755905511810774 ) ) ;
#7056=CARTESIAN_POINT ( 'NONE',  ( 0.4685039370078740717, 0.000000000000000000, 0.4507874015748032370 ) ) ;
#7061=CARTESIAN_POINT ( 'NONE',  ( 0.3432736861146661322, 0.3267484299055463115, 0.02460629921259843353 ) ) ;
#7064=CARTESIAN_POINT ( 'NONE',  ( 0.3581828924050323715, 0.1743168766271109560, 0.3019256869348722616 ) ) ;
#7066=ORIENTED_EDGE ( 'NONE', *, *, #7509, .T. ) ;
#7067=CARTESIAN_POINT ( 'NONE',  ( 0.3426147637089220765, 0.05832033309504411345, -0.3015404986019938893 ) ) ;
#7071=ORIENTED_EDGE ( 'NONE', *, *, #5676, .T. ) ;
#7075=SHAPE_REPRESENTATION ( 'hex flange bolt small_iso_ISO 4162 - M12 x 30 x 30-N', ( #5166 ), #1473 ) ;
#7078=DIRECTION ( 'NONE',  ( -1.000000000000000000, -0.000000000000000000, -0.000000000000000000 ) ) ;
#7090=AXIS2_PLACEMENT_3D ( 'NONE', #5934, #3713, #3170 ) ;
#7097=PRODUCT_DEFINITION_CONTEXT ( 'detailed design', #1435, 'design' ) ;
#7101=CARTESIAN_POINT ( 'NONE',  ( 0.3528971332113847725, -0.1886393090946611450, -0.2768874834731246404 ) ) ;
#7103=EDGE_CURVE ( 'NONE', #6925, #6629, #748, .T. ) ;
#7108=FACE_OUTER_BOUND ( 'NONE', #5411, .T. ) ;
#7110=DIRECTION ( 'NONE',  ( -0.7071067811865523467, 0.000000000000000000, 0.7071067811865426878 ) ) ;
#7131=CARTESIAN_POINT ( 'NONE',  ( 0.0006233585804810778822, -0.2702164766613439628, -0.1225225144826657953 ) ) ;
#7143=ADVANCED_FACE ( 'NONE', ( #3134 ), #4726, .F. ) ;
#7147=EDGE_CURVE ( 'NONE', #1388, #4696, #4938, .T. ) ;
#7150=DIRECTION ( 'NONE',  ( 0.000000000000000000, 0.000000000000000000, -1.000000000000000000 ) ) ;
#7165=CARTESIAN_POINT ( 'NONE',  ( 0.3398312250858251948, -0.3151631602416472555, -0.04467257488985885983 ) ) ;
#7177=CARTESIAN_POINT ( 'NONE',  ( 0.000000000000000000, 0.000000000000000000, 0.000000000000000000 ) ) ;
#7184=CARTESIAN_POINT ( 'NONE',  ( 0.01168997831664882192, -0.1984671517595423818, -0.2467959906213527677 ) ) ;
#7194=CARTESIAN_POINT ( 'NONE',  ( 0.3565422270302657237, 0.3441025489056184772, -0.005451916616122978385 ) ) ;
#7197=AXIS2_PLACEMENT_3D ( 'NONE', #1458, #826, #3809 ) ;
#7198=EDGE_CURVE ( 'NONE', #6087, #4293, #2220, .T. ) ;
#7199=ORIENTED_EDGE ( 'NONE', *, *, #2928, .T. ) ;
#7207=CARTESIAN_POINT ( 'NONE',  ( 0.3410249605999410294, -1.062517223525361548E-12, -0.3014927230551905368 ) ) ;
#7212=CARTESIAN_POINT ( 'NONE',  ( 0.3426404862726870615, 0.2318193597401792261, 0.2015595396344879719 ) ) ;
#7231=CONICAL_SURFACE ( 'NONE', #640, 0.2952755905511810774, 1.047197551196600518 ) ;
#7234=CARTESIAN_POINT ( 'NONE',  ( 0.3398312250857989381, 0.3151631602416481437, 0.04467257488985636182 ) ) ;
#7250=EDGE_CURVE ( 'NONE', #6209, #2382, #3471, .T. ) ;
#7251=CARTESIAN_POINT ( 'NONE',  ( 0.3432736861146659657, -0.1420645347415416260, 0.2952755905511810774 ) ) ;
#7254=ORIENTED_EDGE ( 'NONE', *, *, #1336, .F. ) ;
#7259=DIRECTION ( 'NONE',  ( -0.7071067811865523467, 8.659560562354873694E-17, -0.7071067811865426878 ) ) ;
#7262=VERTEX_POINT ( 'NONE', #32 ) ;
#7266=CARTESIAN_POINT ( 'NONE',  ( 0.4685039370078740717, 0.1704774416898499345, 0.2952755905511810774 ) ) ;
#7272=ORIENTED_EDGE ( 'NONE', *, *, #3088, .F. ) ;
#7293=DIRECTION ( 'NONE',  ( 0.3420201433256623291, 0.000000000000000000, -0.9396926207859106484 ) ) ;
#7294=AXIS2_PLACEMENT_3D ( 'NONE', #919, #2562, #241 ) ;
#7315=( CONVERSION_BASED_UNIT ( 'INCH', #2654 ) LENGTH_UNIT ( ) NAMED_UNIT ( #5759 ) );
#7323=CARTESIAN_POINT ( 'NONE',  ( 0.0006233585804808155053, 0.2702164766613434077, 0.1225225144826656842 ) ) ;
#7325=VERTEX_POINT ( 'NONE', #2392 ) ;
#7326=DIRECTION ( 'NONE',  ( 0.000000000000000000, -0.5000000000000012212, -0.8660254037844377084 ) ) ;
#7329=ADVANCED_FACE ( 'NONE', ( #3544 ), #66, .F. ) ;
#7335=CARTESIAN_POINT ( 'NONE',  ( 0.3574299024618896592, -0.1732824651941382854, 0.3001340337771306044 ) ) ;
#7336=AXIS2_PLACEMENT_3D ( 'NONE', #6693, #3863, #1440 ) ;
#7340=EDGE_CURVE ( 'NONE', #5905, #2762, #115, .T. ) ;
#7349=CARTESIAN_POINT ( 'NONE',  ( 1.611653543307086212, 2.892866454678787531E-17, -0.2362204724409449064 ) ) ;
#7361=CARTESIAN_POINT ( 'NONE',  ( 0.3581828924050323715, 0.1743168766271107895, -0.3019256869348722061 ) ) ;
#7362=CYLINDRICAL_SURFACE ( 'NONE', #7414, 0.2362204724409449064 ) ;
#7364=FACE_OUTER_BOUND ( 'NONE', #6391, .T. ) ;
#7365=VECTOR ( 'NONE', #6302, 39.37007874015748143 ) ;
#7383=CARTESIAN_POINT ( 'NONE',  ( 0.3391892065151629332, -0.1988903486381584651, 0.2460629921259843145 ) ) ;
#7384=ORIENTED_EDGE ( 'NONE', *, *, #1880, .T. ) ;
#7394=CARTESIAN_POINT ( 'NONE',  ( 0.3581828924050324825, -0.1743168766271116221, -0.3019256869348722061 ) ) ;
#7404=B_SPLINE_CURVE_WITH_KNOTS ( 'NONE', 3,
 ( #5584, #4536, #3969, #4577, #6297, #5733, #6906, #6152 ),
 .UNSPECIFIED., .F., .F.,
 ( 4, 2, 2, 4 ),
 ( 0.004381617662950723809, 0.005472867551409551883, 0.006564117439868379089, 0.008746617216786035237 ),
 .UNSPECIFIED. ) ;
#7406=DIRECTION ( 'NONE',  ( 0.000000000000000000, 0.000000000000000000, -1.000000000000000000 ) ) ;
#7412=CARTESIAN_POINT ( 'NONE',  ( 0.3403864257300893703, -0.2263128404110642256, 0.1985658431051765538 ) ) ;
#7414=AXIS2_PLACEMENT_3D ( 'NONE', #4544, #6229, #2814 ) ;
#7445=CARTESIAN_POINT ( 'NONE',  ( 0.3483227611829848303, -0.1704774416898505729, -0.2952755905511810774 ) ) ;
#7446=VERTEX_POINT ( 'NONE', #3161 ) ;
#7447=CARTESIAN_POINT ( 'NONE',  ( 0.3510872220067887683, 0.1819230426404221390, -0.2754512281816320352 ) ) ;
#7457=CARTESIAN_POINT ( 'NONE',  ( -2.403706095987794643E-16, 0.2484822268960368286, -0.1601673393405684265 ) ) ;
#7472=EDGE_CURVE ( 'NONE', #4759, #5905, #1938, .T. ) ;
#7475=PLANE ( 'NONE',  #4679 ) ;
#7486=CARTESIAN_POINT ( 'NONE',  ( 0.3496779274129792059, 0.3447056852546006578, 0.006496579416451838881 ) ) ;
#7509=EDGE_CURVE ( 'NONE', #3761, #4821, #2107, .T. ) ;
#7516=ORIENTED_EDGE ( 'NONE', *, *, #6995, .F. ) ;
#7517=CARTESIAN_POINT ( 'NONE',  ( 1.649606299212598381, 0.000000000000000000, 0.000000000000000000 ) ) ;
#7581=COLOUR_RGB('Black',0.12,0.14,0.17);
#7582=FILL_AREA_STYLE_COLOUR('',#7581);
#7583=FILL_AREA_STYLE('',(#7582));
#7584=SURFACE_STYLE_FILL_AREA(#7583);
#7585=SURFACE_SIDE_STYLE('',(#7584));
#7586=SURFACE_STYLE_USAGE(.BOTH.,#7585);
#7587=PRESENTATION_STYLE_ASSIGNMENT((#7586));
ENDSEC;
END-ISO-10303-21;
